ISO-10303-21;
HEADER;
/* Generated by software containing ST-Developer
 * from STEP Tools, Inc. (www.steptools.com) 
 */

FILE_DESCRIPTION(
/* description */ (''),
/* implementation_level */ '2;1');

FILE_NAME(
/* name */ 'Slider_01 (1).step',
/* time_stamp */ '2026-10-22T15:07:41+06:00',
/* author */ (''),
/* organization */ (''),
/* preprocessor_version */ 'ST-DEVELOPER v20.2',
/* originating_system */ 'Autodesk Translation Framework v15.15.0.0',
/* authorisation */ '');

FILE_SCHEMA (('AUTOMOTIVE_DESIGN { 1 0 10303 214 3 1 1 }'));
ENDSEC;

DATA;
#10=MECHANICAL_DESIGN_GEOMETRIC_PRESENTATION_REPRESENTATION('',(#2882),#19220);
#71=SHAPE_REPRESENTATION_RELATIONSHIP('SRR','None',#19274,#85);
#85=ADVANCED_BREP_SHAPE_REPRESENTATION('',(#99),#19210);
#99=MANIFOLD_SOLID_BREP('Slider_01',#11318);
#185=FACE_BOUND('',#3639,.T.);
#186=FACE_BOUND('',#3641,.T.);
#656=PLANE('',#11685);
#657=PLANE('',#11689);
#658=PLANE('',#11690);
#659=PLANE('',#11694);
#660=PLANE('',#11701);
#661=PLANE('',#11702);
#662=PLANE('',#11706);
#663=PLANE('',#11707);
#664=PLANE('',#11711);
#665=PLANE('',#11715);
#666=PLANE('',#11719);
#667=PLANE('',#11720);
#668=PLANE('',#11721);
#669=PLANE('',#11725);
#670=PLANE('',#11729);
#671=PLANE('',#11730);
#672=PLANE('',#11731);
#673=PLANE('',#11735);
#674=PLANE('',#11739);
#675=PLANE('',#11743);
#676=PLANE('',#11747);
#677=PLANE('',#11748);
#678=PLANE('',#11749);
#679=PLANE('',#11753);
#680=PLANE('',#11757);
#681=PLANE('',#11758);
#929=LINE('',#16502,#1784);
#930=LINE('',#16504,#1785);
#931=LINE('',#16506,#1786);
#932=LINE('',#16507,#1787);
#933=LINE('',#16512,#1788);
#934=LINE('',#16516,#1789);
#935=LINE('',#16518,#1790);
#936=LINE('',#16519,#1791);
#937=LINE('',#16523,#1792);
#938=LINE('',#16525,#1793);
#939=LINE('',#16527,#1794);
#940=LINE('',#16528,#1795);
#941=LINE('',#16533,#1796);
#942=LINE('',#16537,#1797);
#943=LINE('',#16539,#1798);
#944=LINE('',#16540,#1799);
#945=LINE('',#16545,#1800);
#946=LINE('',#16552,#1801);
#947=LINE('',#16555,#1802);
#948=LINE('',#16557,#1803);
#949=LINE('',#16558,#1804);
#950=LINE('',#16562,#1805);
#951=LINE('',#16564,#1806);
#952=LINE('',#16566,#1807);
#953=LINE('',#16567,#1808);
#954=LINE('',#16573,#1809);
#955=LINE('',#16576,#1810);
#956=LINE('',#16578,#1811);
#957=LINE('',#16579,#1812);
#958=LINE('',#16583,#1813);
#959=LINE('',#16585,#1814);
#960=LINE('',#16587,#1815);
#961=LINE('',#16588,#1816);
#962=LINE('',#16594,#1817);
#963=LINE('',#16597,#1818);
#964=LINE('',#16599,#1819);
#965=LINE('',#16600,#1820);
#966=LINE('',#16606,#1821);
#967=LINE('',#16608,#1822);
#968=LINE('',#16609,#1823);
#969=LINE('',#16615,#1824);
#970=LINE('',#16617,#1825);
#971=LINE('',#16618,#1826);
#972=LINE('',#16621,#1827);
#973=LINE('',#16623,#1828);
#974=LINE('',#16624,#1829);
#975=LINE('',#16626,#1830);
#976=LINE('',#16627,#1831);
#977=LINE('',#16632,#1832);
#978=LINE('',#16636,#1833);
#979=LINE('',#16638,#1834);
#980=LINE('',#16639,#1835);
#981=LINE('',#16644,#1836);
#982=LINE('',#16648,#1837);
#983=LINE('',#16650,#1838);
#984=LINE('',#16651,#1839);
#985=LINE('',#16654,#1840);
#986=LINE('',#16656,#1841);
#987=LINE('',#16657,#1842);
#988=LINE('',#16660,#1843);
#989=LINE('',#16662,#1844);
#990=LINE('',#16663,#1845);
#991=LINE('',#16668,#1846);
#992=LINE('',#16672,#1847);
#993=LINE('',#16674,#1848);
#994=LINE('',#16675,#1849);
#995=LINE('',#16680,#1850);
#996=LINE('',#16684,#1851);
#997=LINE('',#16686,#1852);
#998=LINE('',#16687,#1853);
#999=LINE('',#16693,#1854);
#1000=LINE('',#16696,#1855);
#1001=LINE('',#16698,#1856);
#1002=LINE('',#16699,#1857);
#1003=LINE('',#16705,#1858);
#1004=LINE('',#16708,#1859);
#1005=LINE('',#16710,#1860);
#1006=LINE('',#16711,#1861);
#1007=LINE('',#16714,#1862);
#1008=LINE('',#16716,#1863);
#1009=LINE('',#16717,#1864);
#1010=LINE('',#16720,#1865);
#1011=LINE('',#16722,#1866);
#1012=LINE('',#16723,#1867);
#1013=LINE('',#16729,#1868);
#1014=LINE('',#16732,#1869);
#1015=LINE('',#16734,#1870);
#1016=LINE('',#16735,#1871);
#1784=VECTOR('',#13224,10.);
#1785=VECTOR('',#13225,10.);
#1786=VECTOR('',#13226,10.);
#1787=VECTOR('',#13227,10.);
#1788=VECTOR('',#13232,10.);
#1789=VECTOR('',#13237,10.);
#1790=VECTOR('',#13238,10.);
#1791=VECTOR('',#13239,10.);
#1792=VECTOR('',#13242,10.);
#1793=VECTOR('',#13243,10.);
#1794=VECTOR('',#13244,10.);
#1795=VECTOR('',#13245,10.);
#1796=VECTOR('',#13250,10.);
#1797=VECTOR('',#13255,10.);
#1798=VECTOR('',#13256,10.);
#1799=VECTOR('',#13257,10.);
#1800=VECTOR('',#13262,10.);
#1801=VECTOR('',#13271,10.);
#1802=VECTOR('',#13274,10.);
#1803=VECTOR('',#13275,10.);
#1804=VECTOR('',#13276,10.);
#1805=VECTOR('',#13279,10.);
#1806=VECTOR('',#13280,10.);
#1807=VECTOR('',#13281,10.);
#1808=VECTOR('',#13282,10.);
#1809=VECTOR('',#13289,10.);
#1810=VECTOR('',#13292,10.);
#1811=VECTOR('',#13293,10.);
#1812=VECTOR('',#13294,10.);
#1813=VECTOR('',#13297,10.);
#1814=VECTOR('',#13298,10.);
#1815=VECTOR('',#13299,10.);
#1816=VECTOR('',#13300,10.);
#1817=VECTOR('',#13307,10.);
#1818=VECTOR('',#13310,10.);
#1819=VECTOR('',#13311,10.);
#1820=VECTOR('',#13312,10.);
#1821=VECTOR('',#13321,10.);
#1822=VECTOR('',#13322,10.);
#1823=VECTOR('',#13323,10.);
#1824=VECTOR('',#13332,10.);
#1825=VECTOR('',#13333,10.);
#1826=VECTOR('',#13334,10.);
#1827=VECTOR('',#13337,10.);
#1828=VECTOR('',#13338,10.);
#1829=VECTOR('',#13339,10.);
#1830=VECTOR('',#13342,10.);
#1831=VECTOR('',#13343,10.);
#1832=VECTOR('',#13348,10.);
#1833=VECTOR('',#13353,10.);
#1834=VECTOR('',#13354,10.);
#1835=VECTOR('',#13355,10.);
#1836=VECTOR('',#13360,10.);
#1837=VECTOR('',#13365,10.);
#1838=VECTOR('',#13366,10.);
#1839=VECTOR('',#13367,10.);
#1840=VECTOR('',#13370,10.);
#1841=VECTOR('',#13371,10.);
#1842=VECTOR('',#13372,10.);
#1843=VECTOR('',#13375,10.);
#1844=VECTOR('',#13376,10.);
#1845=VECTOR('',#13377,10.);
#1846=VECTOR('',#13382,10.);
#1847=VECTOR('',#13387,10.);
#1848=VECTOR('',#13388,10.);
#1849=VECTOR('',#13389,10.);
#1850=VECTOR('',#13394,10.);
#1851=VECTOR('',#13399,10.);
#1852=VECTOR('',#13400,10.);
#1853=VECTOR('',#13401,10.);
#1854=VECTOR('',#13408,10.);
#1855=VECTOR('',#13411,10.);
#1856=VECTOR('',#13412,10.);
#1857=VECTOR('',#13413,10.);
#1858=VECTOR('',#13420,10.);
#1859=VECTOR('',#13423,10.);
#1860=VECTOR('',#13424,10.);
#1861=VECTOR('',#13425,10.);
#1862=VECTOR('',#13428,10.);
#1863=VECTOR('',#13429,10.);
#1864=VECTOR('',#13430,10.);
#1865=VECTOR('',#13433,10.);
#1866=VECTOR('',#13434,10.);
#1867=VECTOR('',#13435,10.);
#1868=VECTOR('',#13442,10.);
#1869=VECTOR('',#13445,10.);
#1870=VECTOR('',#13446,10.);
#1871=VECTOR('',#13447,10.);
#2597=CYLINDRICAL_SURFACE('',#11686,0.999999999999975);
#2598=CYLINDRICAL_SURFACE('',#11691,1.99999999999998);
#2599=CYLINDRICAL_SURFACE('',#11695,0.500000000000007);
#2600=CYLINDRICAL_SURFACE('',#11698,0.499999999999998);
#2601=CYLINDRICAL_SURFACE('',#11703,0.999999999999975);
#2602=CYLINDRICAL_SURFACE('',#11708,1.99999999999998);
#2603=CYLINDRICAL_SURFACE('',#11712,0.500000000000007);
#2604=CYLINDRICAL_SURFACE('',#11716,0.499999999999998);
#2605=CYLINDRICAL_SURFACE('',#11722,0.999999999999981);
#2606=CYLINDRICAL_SURFACE('',#11726,0.999999999999967);
#2607=CYLINDRICAL_SURFACE('',#11732,1.99999999999997);
#2608=CYLINDRICAL_SURFACE('',#11736,1.99999999999998);
#2609=CYLINDRICAL_SURFACE('',#11740,0.999999999999981);
#2610=CYLINDRICAL_SURFACE('',#11744,0.999999999999967);
#2611=CYLINDRICAL_SURFACE('',#11750,1.99999999999997);
#2612=CYLINDRICAL_SURFACE('',#11754,1.99999999999998);
#2882=STYLED_ITEM('',(#19396),#99);
#2976=FACE_OUTER_BOUND('',#3598,.T.);
#2977=FACE_OUTER_BOUND('',#3599,.T.);
#2978=FACE_OUTER_BOUND('',#3600,.T.);
#2979=FACE_OUTER_BOUND('',#3601,.T.);
#2980=FACE_OUTER_BOUND('',#3602,.T.);
#2981=FACE_OUTER_BOUND('',#3603,.T.);
#2982=FACE_OUTER_BOUND('',#3604,.T.);
#2983=FACE_OUTER_BOUND('',#3605,.T.);
#2984=FACE_OUTER_BOUND('',#3606,.T.);
#2985=FACE_OUTER_BOUND('',#3607,.T.);
#2986=FACE_OUTER_BOUND('',#3608,.T.);
#2987=FACE_OUTER_BOUND('',#3609,.T.);
#2988=FACE_OUTER_BOUND('',#3610,.T.);
#2989=FACE_OUTER_BOUND('',#3611,.T.);
#2990=FACE_OUTER_BOUND('',#3612,.T.);
#2991=FACE_OUTER_BOUND('',#3613,.T.);
#2992=FACE_OUTER_BOUND('',#3614,.T.);
#2993=FACE_OUTER_BOUND('',#3615,.T.);
#2994=FACE_OUTER_BOUND('',#3616,.T.);
#2995=FACE_OUTER_BOUND('',#3617,.T.);
#2996=FACE_OUTER_BOUND('',#3618,.T.);
#2997=FACE_OUTER_BOUND('',#3619,.T.);
#2998=FACE_OUTER_BOUND('',#3620,.T.);
#2999=FACE_OUTER_BOUND('',#3621,.T.);
#3000=FACE_OUTER_BOUND('',#3622,.T.);
#3001=FACE_OUTER_BOUND('',#3623,.T.);
#3002=FACE_OUTER_BOUND('',#3624,.T.);
#3003=FACE_OUTER_BOUND('',#3625,.T.);
#3004=FACE_OUTER_BOUND('',#3626,.T.);
#3005=FACE_OUTER_BOUND('',#3627,.T.);
#3006=FACE_OUTER_BOUND('',#3628,.T.);
#3007=FACE_OUTER_BOUND('',#3629,.T.);
#3008=FACE_OUTER_BOUND('',#3630,.T.);
#3009=FACE_OUTER_BOUND('',#3631,.T.);
#3010=FACE_OUTER_BOUND('',#3632,.T.);
#3011=FACE_OUTER_BOUND('',#3633,.T.);
#3012=FACE_OUTER_BOUND('',#3634,.T.);
#3013=FACE_OUTER_BOUND('',#3635,.T.);
#3014=FACE_OUTER_BOUND('',#3636,.T.);
#3015=FACE_OUTER_BOUND('',#3637,.T.);
#3016=FACE_OUTER_BOUND('',#3638,.T.);
#3017=FACE_OUTER_BOUND('',#3640,.T.);
#3598=EDGE_LOOP('',(#8116,#8117,#8118,#8119));
#3599=EDGE_LOOP('',(#8120,#8121,#8122,#8123));
#3600=EDGE_LOOP('',(#8124,#8125,#8126,#8127));
#3601=EDGE_LOOP('',(#8128,#8129,#8130,#8131));
#3602=EDGE_LOOP('',(#8132,#8133,#8134,#8135));
#3603=EDGE_LOOP('',(#8136,#8137,#8138,#8139));
#3604=EDGE_LOOP('',(#8140,#8141,#8142,#8143));
#3605=EDGE_LOOP('',(#8144,#8145,#8146,#8147));
#3606=EDGE_LOOP('',(#8148,#8149,#8150,#8151));
#3607=EDGE_LOOP('',(#8152,#8153,#8154,#8155));
#3608=EDGE_LOOP('',(#8156,#8157,#8158,#8159));
#3609=EDGE_LOOP('',(#8160,#8161,#8162,#8163));
#3610=EDGE_LOOP('',(#8164,#8165,#8166,#8167));
#3611=EDGE_LOOP('',(#8168,#8169,#8170,#8171));
#3612=EDGE_LOOP('',(#8172,#8173,#8174,#8175));
#3613=EDGE_LOOP('',(#8176,#8177,#8178,#8179));
#3614=EDGE_LOOP('',(#8180,#8181,#8182,#8183));
#3615=EDGE_LOOP('',(#8184,#8185,#8186,#8187));
#3616=EDGE_LOOP('',(#8188,#8189,#8190,#8191));
#3617=EDGE_LOOP('',(#8192,#8193,#8194,#8195));
#3618=EDGE_LOOP('',(#8196,#8197,#8198,#8199));
#3619=EDGE_LOOP('',(#8200,#8201,#8202,#8203));
#3620=EDGE_LOOP('',(#8204,#8205,#8206,#8207));
#3621=EDGE_LOOP('',(#8208,#8209,#8210,#8211));
#3622=EDGE_LOOP('',(#8212,#8213,#8214,#8215));
#3623=EDGE_LOOP('',(#8216,#8217,#8218,#8219));
#3624=EDGE_LOOP('',(#8220,#8221,#8222,#8223));
#3625=EDGE_LOOP('',(#8224,#8225,#8226,#8227));
#3626=EDGE_LOOP('',(#8228,#8229,#8230,#8231));
#3627=EDGE_LOOP('',(#8232,#8233,#8234,#8235));
#3628=EDGE_LOOP('',(#8236,#8237,#8238,#8239));
#3629=EDGE_LOOP('',(#8240,#8241,#8242,#8243));
#3630=EDGE_LOOP('',(#8244,#8245,#8246,#8247));
#3631=EDGE_LOOP('',(#8248,#8249,#8250,#8251));
#3632=EDGE_LOOP('',(#8252,#8253,#8254,#8255));
#3633=EDGE_LOOP('',(#8256,#8257,#8258,#8259));
#3634=EDGE_LOOP('',(#8260,#8261,#8262,#8263));
#3635=EDGE_LOOP('',(#8264,#8265,#8266,#8267));
#3636=EDGE_LOOP('',(#8268,#8269,#8270,#8271));
#3637=EDGE_LOOP('',(#8272,#8273,#8274,#8275));
#3638=EDGE_LOOP('',(#8276,#8277,#8278,#8279,#8280,#8281,#8282,#8283,#8284,
#8285,#8286,#8287,#8288,#8289,#8290,#8291,#8292,#8293,#8294,#8295,#8296,
#8297,#8298,#8299,#8300,#8301,#8302,#8303,#8304,#8305));
#3639=EDGE_LOOP('',(#8306,#8307,#8308,#8309,#8310,#8311,#8312,#8313,#8314,
#8315));
#3640=EDGE_LOOP('',(#8316,#8317,#8318,#8319,#8320,#8321,#8322,#8323,#8324,
#8325,#8326,#8327,#8328,#8329,#8330,#8331,#8332,#8333,#8334,#8335,#8336,
#8337,#8338,#8339,#8340,#8341,#8342,#8343,#8344,#8345));
#3641=EDGE_LOOP('',(#8346,#8347,#8348,#8349,#8350,#8351,#8352,#8353,#8354,
#8355));
#4613=CIRCLE('',#11687,0.999999999999975);
#4614=CIRCLE('',#11688,0.999999999999975);
#4615=CIRCLE('',#11692,1.99999999999998);
#4616=CIRCLE('',#11693,1.99999999999998);
#4617=CIRCLE('',#11696,0.500000000000007);
#4618=CIRCLE('',#11697,0.500000000000007);
#4619=CIRCLE('',#11699,0.499999999999998);
#4620=CIRCLE('',#11700,0.499999999999998);
#4621=CIRCLE('',#11704,0.999999999999975);
#4622=CIRCLE('',#11705,0.999999999999975);
#4623=CIRCLE('',#11709,1.99999999999998);
#4624=CIRCLE('',#11710,1.99999999999998);
#4625=CIRCLE('',#11713,0.500000000000007);
#4626=CIRCLE('',#11714,0.500000000000007);
#4627=CIRCLE('',#11717,0.499999999999998);
#4628=CIRCLE('',#11718,0.499999999999998);
#4629=CIRCLE('',#11723,0.999999999999981);
#4630=CIRCLE('',#11724,0.999999999999981);
#4631=CIRCLE('',#11727,0.999999999999967);
#4632=CIRCLE('',#11728,0.999999999999967);
#4633=CIRCLE('',#11733,1.99999999999997);
#4634=CIRCLE('',#11734,1.99999999999997);
#4635=CIRCLE('',#11737,1.99999999999998);
#4636=CIRCLE('',#11738,1.99999999999998);
#4637=CIRCLE('',#11741,0.999999999999981);
#4638=CIRCLE('',#11742,0.999999999999981);
#4639=CIRCLE('',#11745,0.999999999999967);
#4640=CIRCLE('',#11746,0.999999999999967);
#4641=CIRCLE('',#11751,1.99999999999997);
#4642=CIRCLE('',#11752,1.99999999999997);
#4643=CIRCLE('',#11755,1.99999999999998);
#4644=CIRCLE('',#11756,1.99999999999998);
#5305=VERTEX_POINT('',#16500);
#5306=VERTEX_POINT('',#16501);
#5307=VERTEX_POINT('',#16503);
#5308=VERTEX_POINT('',#16505);
#5309=VERTEX_POINT('',#16509);
#5310=VERTEX_POINT('',#16511);
#5311=VERTEX_POINT('',#16515);
#5312=VERTEX_POINT('',#16517);
#5313=VERTEX_POINT('',#16521);
#5314=VERTEX_POINT('',#16522);
#5315=VERTEX_POINT('',#16524);
#5316=VERTEX_POINT('',#16526);
#5317=VERTEX_POINT('',#16530);
#5318=VERTEX_POINT('',#16532);
#5319=VERTEX_POINT('',#16536);
#5320=VERTEX_POINT('',#16538);
#5321=VERTEX_POINT('',#16542);
#5322=VERTEX_POINT('',#16544);
#5323=VERTEX_POINT('',#16548);
#5324=VERTEX_POINT('',#16550);
#5325=VERTEX_POINT('',#16554);
#5326=VERTEX_POINT('',#16556);
#5327=VERTEX_POINT('',#16560);
#5328=VERTEX_POINT('',#16561);
#5329=VERTEX_POINT('',#16563);
#5330=VERTEX_POINT('',#16565);
#5331=VERTEX_POINT('',#16569);
#5332=VERTEX_POINT('',#16571);
#5333=VERTEX_POINT('',#16575);
#5334=VERTEX_POINT('',#16577);
#5335=VERTEX_POINT('',#16581);
#5336=VERTEX_POINT('',#16582);
#5337=VERTEX_POINT('',#16584);
#5338=VERTEX_POINT('',#16586);
#5339=VERTEX_POINT('',#16590);
#5340=VERTEX_POINT('',#16592);
#5341=VERTEX_POINT('',#16596);
#5342=VERTEX_POINT('',#16598);
#5343=VERTEX_POINT('',#16605);
#5344=VERTEX_POINT('',#16607);
#5345=VERTEX_POINT('',#16614);
#5346=VERTEX_POINT('',#16616);
#5347=VERTEX_POINT('',#16620);
#5348=VERTEX_POINT('',#16622);
#5349=VERTEX_POINT('',#16629);
#5350=VERTEX_POINT('',#16631);
#5351=VERTEX_POINT('',#16635);
#5352=VERTEX_POINT('',#16637);
#5353=VERTEX_POINT('',#16641);
#5354=VERTEX_POINT('',#16643);
#5355=VERTEX_POINT('',#16647);
#5356=VERTEX_POINT('',#16649);
#5357=VERTEX_POINT('',#16653);
#5358=VERTEX_POINT('',#16655);
#5359=VERTEX_POINT('',#16659);
#5360=VERTEX_POINT('',#16661);
#5361=VERTEX_POINT('',#16665);
#5362=VERTEX_POINT('',#16667);
#5363=VERTEX_POINT('',#16671);
#5364=VERTEX_POINT('',#16673);
#5365=VERTEX_POINT('',#16677);
#5366=VERTEX_POINT('',#16679);
#5367=VERTEX_POINT('',#16683);
#5368=VERTEX_POINT('',#16685);
#5369=VERTEX_POINT('',#16689);
#5370=VERTEX_POINT('',#16691);
#5371=VERTEX_POINT('',#16695);
#5372=VERTEX_POINT('',#16697);
#5373=VERTEX_POINT('',#16701);
#5374=VERTEX_POINT('',#16703);
#5375=VERTEX_POINT('',#16707);
#5376=VERTEX_POINT('',#16709);
#5377=VERTEX_POINT('',#16713);
#5378=VERTEX_POINT('',#16715);
#5379=VERTEX_POINT('',#16719);
#5380=VERTEX_POINT('',#16721);
#5381=VERTEX_POINT('',#16725);
#5382=VERTEX_POINT('',#16727);
#5383=VERTEX_POINT('',#16731);
#5384=VERTEX_POINT('',#16733);
#6389=EDGE_CURVE('',#5305,#5306,#929,.T.);
#6390=EDGE_CURVE('',#5306,#5307,#930,.T.);
#6391=EDGE_CURVE('',#5307,#5308,#931,.T.);
#6392=EDGE_CURVE('',#5305,#5308,#932,.T.);
#6393=EDGE_CURVE('',#5309,#5306,#4613,.T.);
#6394=EDGE_CURVE('',#5309,#5310,#933,.T.);
#6395=EDGE_CURVE('',#5310,#5307,#4614,.T.);
#6396=EDGE_CURVE('',#5309,#5311,#934,.T.);
#6397=EDGE_CURVE('',#5312,#5311,#935,.T.);
#6398=EDGE_CURVE('',#5312,#5310,#936,.T.);
#6399=EDGE_CURVE('',#5313,#5314,#937,.T.);
#6400=EDGE_CURVE('',#5313,#5315,#938,.T.);
#6401=EDGE_CURVE('',#5315,#5316,#939,.T.);
#6402=EDGE_CURVE('',#5314,#5316,#940,.T.);
#6403=EDGE_CURVE('',#5313,#5317,#4615,.T.);
#6404=EDGE_CURVE('',#5317,#5318,#941,.T.);
#6405=EDGE_CURVE('',#5318,#5315,#4616,.T.);
#6406=EDGE_CURVE('',#5319,#5317,#942,.T.);
#6407=EDGE_CURVE('',#5319,#5320,#943,.T.);
#6408=EDGE_CURVE('',#5320,#5318,#944,.T.);
#6409=EDGE_CURVE('',#5321,#5319,#4617,.T.);
#6410=EDGE_CURVE('',#5321,#5322,#945,.T.);
#6411=EDGE_CURVE('',#5322,#5320,#4618,.T.);
#6412=EDGE_CURVE('',#5323,#5305,#4619,.T.);
#6413=EDGE_CURVE('',#5308,#5324,#4620,.T.);
#6414=EDGE_CURVE('',#5323,#5324,#946,.T.);
#6415=EDGE_CURVE('',#5321,#5325,#947,.T.);
#6416=EDGE_CURVE('',#5325,#5326,#948,.T.);
#6417=EDGE_CURVE('',#5326,#5322,#949,.T.);
#6418=EDGE_CURVE('',#5327,#5328,#950,.T.);
#6419=EDGE_CURVE('',#5327,#5329,#951,.T.);
#6420=EDGE_CURVE('',#5330,#5329,#952,.T.);
#6421=EDGE_CURVE('',#5328,#5330,#953,.T.);
#6422=EDGE_CURVE('',#5331,#5328,#4621,.T.);
#6423=EDGE_CURVE('',#5332,#5330,#4622,.T.);
#6424=EDGE_CURVE('',#5331,#5332,#954,.T.);
#6425=EDGE_CURVE('',#5331,#5333,#955,.T.);
#6426=EDGE_CURVE('',#5334,#5332,#956,.T.);
#6427=EDGE_CURVE('',#5333,#5334,#957,.T.);
#6428=EDGE_CURVE('',#5335,#5336,#958,.T.);
#6429=EDGE_CURVE('',#5337,#5336,#959,.T.);
#6430=EDGE_CURVE('',#5338,#5337,#960,.T.);
#6431=EDGE_CURVE('',#5335,#5338,#961,.T.);
#6432=EDGE_CURVE('',#5335,#5339,#4623,.T.);
#6433=EDGE_CURVE('',#5340,#5338,#4624,.T.);
#6434=EDGE_CURVE('',#5339,#5340,#962,.T.);
#6435=EDGE_CURVE('',#5341,#5339,#963,.T.);
#6436=EDGE_CURVE('',#5342,#5340,#964,.T.);
#6437=EDGE_CURVE('',#5341,#5342,#965,.T.);
#6438=EDGE_CURVE('',#5325,#5341,#4625,.T.);
#6439=EDGE_CURVE('',#5326,#5342,#4626,.T.);
#6440=EDGE_CURVE('',#5343,#5324,#966,.T.);
#6441=EDGE_CURVE('',#5344,#5343,#967,.T.);
#6442=EDGE_CURVE('',#5323,#5344,#968,.T.);
#6443=EDGE_CURVE('',#5344,#5327,#4627,.T.);
#6444=EDGE_CURVE('',#5329,#5343,#4628,.T.);
#6445=EDGE_CURVE('',#5345,#5334,#969,.T.);
#6446=EDGE_CURVE('',#5346,#5345,#970,.T.);
#6447=EDGE_CURVE('',#5346,#5333,#971,.T.);
#6448=EDGE_CURVE('',#5311,#5347,#972,.T.);
#6449=EDGE_CURVE('',#5347,#5348,#973,.T.);
#6450=EDGE_CURVE('',#5312,#5348,#974,.T.);
#6451=EDGE_CURVE('',#5337,#5316,#975,.T.);
#6452=EDGE_CURVE('',#5336,#5314,#976,.T.);
#6453=EDGE_CURVE('',#5349,#5347,#4629,.T.);
#6454=EDGE_CURVE('',#5349,#5350,#977,.T.);
#6455=EDGE_CURVE('',#5350,#5348,#4630,.T.);
#6456=EDGE_CURVE('',#5349,#5351,#978,.T.);
#6457=EDGE_CURVE('',#5351,#5352,#979,.T.);
#6458=EDGE_CURVE('',#5352,#5350,#980,.T.);
#6459=EDGE_CURVE('',#5353,#5351,#4631,.T.);
#6460=EDGE_CURVE('',#5353,#5354,#981,.T.);
#6461=EDGE_CURVE('',#5354,#5352,#4632,.T.);
#6462=EDGE_CURVE('',#5353,#5355,#982,.T.);
#6463=EDGE_CURVE('',#5355,#5356,#983,.T.);
#6464=EDGE_CURVE('',#5356,#5354,#984,.T.);
#6465=EDGE_CURVE('',#5357,#5355,#985,.T.);
#6466=EDGE_CURVE('',#5357,#5358,#986,.T.);
#6467=EDGE_CURVE('',#5358,#5356,#987,.T.);
#6468=EDGE_CURVE('',#5359,#5357,#988,.T.);
#6469=EDGE_CURVE('',#5359,#5360,#989,.T.);
#6470=EDGE_CURVE('',#5360,#5358,#990,.T.);
#6471=EDGE_CURVE('',#5359,#5361,#4633,.T.);
#6472=EDGE_CURVE('',#5361,#5362,#991,.T.);
#6473=EDGE_CURVE('',#5362,#5360,#4634,.T.);
#6474=EDGE_CURVE('',#5363,#5361,#992,.T.);
#6475=EDGE_CURVE('',#5363,#5364,#993,.T.);
#6476=EDGE_CURVE('',#5364,#5362,#994,.T.);
#6477=EDGE_CURVE('',#5363,#5365,#4635,.T.);
#6478=EDGE_CURVE('',#5365,#5366,#995,.T.);
#6479=EDGE_CURVE('',#5366,#5364,#4636,.T.);
#6480=EDGE_CURVE('',#5365,#5367,#996,.T.);
#6481=EDGE_CURVE('',#5367,#5368,#997,.T.);
#6482=EDGE_CURVE('',#5368,#5366,#998,.T.);
#6483=EDGE_CURVE('',#5369,#5346,#4637,.T.);
#6484=EDGE_CURVE('',#5370,#5345,#4638,.T.);
#6485=EDGE_CURVE('',#5369,#5370,#999,.T.);
#6486=EDGE_CURVE('',#5369,#5371,#1000,.T.);
#6487=EDGE_CURVE('',#5372,#5370,#1001,.T.);
#6488=EDGE_CURVE('',#5371,#5372,#1002,.T.);
#6489=EDGE_CURVE('',#5373,#5371,#4639,.T.);
#6490=EDGE_CURVE('',#5374,#5372,#4640,.T.);
#6491=EDGE_CURVE('',#5373,#5374,#1003,.T.);
#6492=EDGE_CURVE('',#5373,#5375,#1004,.T.);
#6493=EDGE_CURVE('',#5376,#5374,#1005,.T.);
#6494=EDGE_CURVE('',#5375,#5376,#1006,.T.);
#6495=EDGE_CURVE('',#5377,#5375,#1007,.T.);
#6496=EDGE_CURVE('',#5378,#5376,#1008,.T.);
#6497=EDGE_CURVE('',#5377,#5378,#1009,.T.);
#6498=EDGE_CURVE('',#5379,#5377,#1010,.T.);
#6499=EDGE_CURVE('',#5380,#5378,#1011,.T.);
#6500=EDGE_CURVE('',#5379,#5380,#1012,.T.);
#6501=EDGE_CURVE('',#5379,#5381,#4641,.T.);
#6502=EDGE_CURVE('',#5382,#5380,#4642,.T.);
#6503=EDGE_CURVE('',#5381,#5382,#1013,.T.);
#6504=EDGE_CURVE('',#5383,#5381,#1014,.T.);
#6505=EDGE_CURVE('',#5384,#5382,#1015,.T.);
#6506=EDGE_CURVE('',#5383,#5384,#1016,.T.);
#6507=EDGE_CURVE('',#5383,#5367,#4643,.T.);
#6508=EDGE_CURVE('',#5368,#5384,#4644,.T.);
#8116=ORIENTED_EDGE('',*,*,#6389,.T.);
#8117=ORIENTED_EDGE('',*,*,#6390,.T.);
#8118=ORIENTED_EDGE('',*,*,#6391,.T.);
#8119=ORIENTED_EDGE('',*,*,#6392,.F.);
#8120=ORIENTED_EDGE('',*,*,#6393,.F.);
#8121=ORIENTED_EDGE('',*,*,#6394,.T.);
#8122=ORIENTED_EDGE('',*,*,#6395,.T.);
#8123=ORIENTED_EDGE('',*,*,#6390,.F.);
#8124=ORIENTED_EDGE('',*,*,#6396,.T.);
#8125=ORIENTED_EDGE('',*,*,#6397,.F.);
#8126=ORIENTED_EDGE('',*,*,#6398,.T.);
#8127=ORIENTED_EDGE('',*,*,#6394,.F.);
#8128=ORIENTED_EDGE('',*,*,#6399,.F.);
#8129=ORIENTED_EDGE('',*,*,#6400,.T.);
#8130=ORIENTED_EDGE('',*,*,#6401,.T.);
#8131=ORIENTED_EDGE('',*,*,#6402,.F.);
#8132=ORIENTED_EDGE('',*,*,#6403,.T.);
#8133=ORIENTED_EDGE('',*,*,#6404,.T.);
#8134=ORIENTED_EDGE('',*,*,#6405,.T.);
#8135=ORIENTED_EDGE('',*,*,#6400,.F.);
#8136=ORIENTED_EDGE('',*,*,#6406,.F.);
#8137=ORIENTED_EDGE('',*,*,#6407,.T.);
#8138=ORIENTED_EDGE('',*,*,#6408,.T.);
#8139=ORIENTED_EDGE('',*,*,#6404,.F.);
#8140=ORIENTED_EDGE('',*,*,#6409,.F.);
#8141=ORIENTED_EDGE('',*,*,#6410,.T.);
#8142=ORIENTED_EDGE('',*,*,#6411,.T.);
#8143=ORIENTED_EDGE('',*,*,#6407,.F.);
#8144=ORIENTED_EDGE('',*,*,#6412,.T.);
#8145=ORIENTED_EDGE('',*,*,#6392,.T.);
#8146=ORIENTED_EDGE('',*,*,#6413,.T.);
#8147=ORIENTED_EDGE('',*,*,#6414,.F.);
#8148=ORIENTED_EDGE('',*,*,#6415,.T.);
#8149=ORIENTED_EDGE('',*,*,#6416,.T.);
#8150=ORIENTED_EDGE('',*,*,#6417,.T.);
#8151=ORIENTED_EDGE('',*,*,#6410,.F.);
#8152=ORIENTED_EDGE('',*,*,#6418,.F.);
#8153=ORIENTED_EDGE('',*,*,#6419,.T.);
#8154=ORIENTED_EDGE('',*,*,#6420,.F.);
#8155=ORIENTED_EDGE('',*,*,#6421,.F.);
#8156=ORIENTED_EDGE('',*,*,#6422,.T.);
#8157=ORIENTED_EDGE('',*,*,#6421,.T.);
#8158=ORIENTED_EDGE('',*,*,#6423,.F.);
#8159=ORIENTED_EDGE('',*,*,#6424,.F.);
#8160=ORIENTED_EDGE('',*,*,#6425,.F.);
#8161=ORIENTED_EDGE('',*,*,#6424,.T.);
#8162=ORIENTED_EDGE('',*,*,#6426,.F.);
#8163=ORIENTED_EDGE('',*,*,#6427,.F.);
#8164=ORIENTED_EDGE('',*,*,#6428,.T.);
#8165=ORIENTED_EDGE('',*,*,#6429,.F.);
#8166=ORIENTED_EDGE('',*,*,#6430,.F.);
#8167=ORIENTED_EDGE('',*,*,#6431,.F.);
#8168=ORIENTED_EDGE('',*,*,#6432,.F.);
#8169=ORIENTED_EDGE('',*,*,#6431,.T.);
#8170=ORIENTED_EDGE('',*,*,#6433,.F.);
#8171=ORIENTED_EDGE('',*,*,#6434,.F.);
#8172=ORIENTED_EDGE('',*,*,#6435,.T.);
#8173=ORIENTED_EDGE('',*,*,#6434,.T.);
#8174=ORIENTED_EDGE('',*,*,#6436,.F.);
#8175=ORIENTED_EDGE('',*,*,#6437,.F.);
#8176=ORIENTED_EDGE('',*,*,#6438,.T.);
#8177=ORIENTED_EDGE('',*,*,#6437,.T.);
#8178=ORIENTED_EDGE('',*,*,#6439,.F.);
#8179=ORIENTED_EDGE('',*,*,#6416,.F.);
#8180=ORIENTED_EDGE('',*,*,#6440,.F.);
#8181=ORIENTED_EDGE('',*,*,#6441,.F.);
#8182=ORIENTED_EDGE('',*,*,#6442,.F.);
#8183=ORIENTED_EDGE('',*,*,#6414,.T.);
#8184=ORIENTED_EDGE('',*,*,#6443,.F.);
#8185=ORIENTED_EDGE('',*,*,#6441,.T.);
#8186=ORIENTED_EDGE('',*,*,#6444,.F.);
#8187=ORIENTED_EDGE('',*,*,#6419,.F.);
#8188=ORIENTED_EDGE('',*,*,#6427,.T.);
#8189=ORIENTED_EDGE('',*,*,#6445,.F.);
#8190=ORIENTED_EDGE('',*,*,#6446,.F.);
#8191=ORIENTED_EDGE('',*,*,#6447,.T.);
#8192=ORIENTED_EDGE('',*,*,#6397,.T.);
#8193=ORIENTED_EDGE('',*,*,#6448,.T.);
#8194=ORIENTED_EDGE('',*,*,#6449,.T.);
#8195=ORIENTED_EDGE('',*,*,#6450,.F.);
#8196=ORIENTED_EDGE('',*,*,#6402,.T.);
#8197=ORIENTED_EDGE('',*,*,#6451,.F.);
#8198=ORIENTED_EDGE('',*,*,#6429,.T.);
#8199=ORIENTED_EDGE('',*,*,#6452,.T.);
#8200=ORIENTED_EDGE('',*,*,#6453,.F.);
#8201=ORIENTED_EDGE('',*,*,#6454,.T.);
#8202=ORIENTED_EDGE('',*,*,#6455,.T.);
#8203=ORIENTED_EDGE('',*,*,#6449,.F.);
#8204=ORIENTED_EDGE('',*,*,#6456,.T.);
#8205=ORIENTED_EDGE('',*,*,#6457,.T.);
#8206=ORIENTED_EDGE('',*,*,#6458,.T.);
#8207=ORIENTED_EDGE('',*,*,#6454,.F.);
#8208=ORIENTED_EDGE('',*,*,#6459,.F.);
#8209=ORIENTED_EDGE('',*,*,#6460,.T.);
#8210=ORIENTED_EDGE('',*,*,#6461,.T.);
#8211=ORIENTED_EDGE('',*,*,#6457,.F.);
#8212=ORIENTED_EDGE('',*,*,#6462,.T.);
#8213=ORIENTED_EDGE('',*,*,#6463,.T.);
#8214=ORIENTED_EDGE('',*,*,#6464,.T.);
#8215=ORIENTED_EDGE('',*,*,#6460,.F.);
#8216=ORIENTED_EDGE('',*,*,#6465,.F.);
#8217=ORIENTED_EDGE('',*,*,#6466,.T.);
#8218=ORIENTED_EDGE('',*,*,#6467,.T.);
#8219=ORIENTED_EDGE('',*,*,#6463,.F.);
#8220=ORIENTED_EDGE('',*,*,#6468,.F.);
#8221=ORIENTED_EDGE('',*,*,#6469,.T.);
#8222=ORIENTED_EDGE('',*,*,#6470,.T.);
#8223=ORIENTED_EDGE('',*,*,#6466,.F.);
#8224=ORIENTED_EDGE('',*,*,#6471,.T.);
#8225=ORIENTED_EDGE('',*,*,#6472,.T.);
#8226=ORIENTED_EDGE('',*,*,#6473,.T.);
#8227=ORIENTED_EDGE('',*,*,#6469,.F.);
#8228=ORIENTED_EDGE('',*,*,#6474,.F.);
#8229=ORIENTED_EDGE('',*,*,#6475,.T.);
#8230=ORIENTED_EDGE('',*,*,#6476,.T.);
#8231=ORIENTED_EDGE('',*,*,#6472,.F.);
#8232=ORIENTED_EDGE('',*,*,#6477,.T.);
#8233=ORIENTED_EDGE('',*,*,#6478,.T.);
#8234=ORIENTED_EDGE('',*,*,#6479,.T.);
#8235=ORIENTED_EDGE('',*,*,#6475,.F.);
#8236=ORIENTED_EDGE('',*,*,#6480,.T.);
#8237=ORIENTED_EDGE('',*,*,#6481,.T.);
#8238=ORIENTED_EDGE('',*,*,#6482,.T.);
#8239=ORIENTED_EDGE('',*,*,#6478,.F.);
#8240=ORIENTED_EDGE('',*,*,#6483,.T.);
#8241=ORIENTED_EDGE('',*,*,#6446,.T.);
#8242=ORIENTED_EDGE('',*,*,#6484,.F.);
#8243=ORIENTED_EDGE('',*,*,#6485,.F.);
#8244=ORIENTED_EDGE('',*,*,#6486,.F.);
#8245=ORIENTED_EDGE('',*,*,#6485,.T.);
#8246=ORIENTED_EDGE('',*,*,#6487,.F.);
#8247=ORIENTED_EDGE('',*,*,#6488,.F.);
#8248=ORIENTED_EDGE('',*,*,#6489,.T.);
#8249=ORIENTED_EDGE('',*,*,#6488,.T.);
#8250=ORIENTED_EDGE('',*,*,#6490,.F.);
#8251=ORIENTED_EDGE('',*,*,#6491,.F.);
#8252=ORIENTED_EDGE('',*,*,#6492,.F.);
#8253=ORIENTED_EDGE('',*,*,#6491,.T.);
#8254=ORIENTED_EDGE('',*,*,#6493,.F.);
#8255=ORIENTED_EDGE('',*,*,#6494,.F.);
#8256=ORIENTED_EDGE('',*,*,#6495,.T.);
#8257=ORIENTED_EDGE('',*,*,#6494,.T.);
#8258=ORIENTED_EDGE('',*,*,#6496,.F.);
#8259=ORIENTED_EDGE('',*,*,#6497,.F.);
#8260=ORIENTED_EDGE('',*,*,#6498,.T.);
#8261=ORIENTED_EDGE('',*,*,#6497,.T.);
#8262=ORIENTED_EDGE('',*,*,#6499,.F.);
#8263=ORIENTED_EDGE('',*,*,#6500,.F.);
#8264=ORIENTED_EDGE('',*,*,#6501,.F.);
#8265=ORIENTED_EDGE('',*,*,#6500,.T.);
#8266=ORIENTED_EDGE('',*,*,#6502,.F.);
#8267=ORIENTED_EDGE('',*,*,#6503,.F.);
#8268=ORIENTED_EDGE('',*,*,#6504,.T.);
#8269=ORIENTED_EDGE('',*,*,#6503,.T.);
#8270=ORIENTED_EDGE('',*,*,#6505,.F.);
#8271=ORIENTED_EDGE('',*,*,#6506,.F.);
#8272=ORIENTED_EDGE('',*,*,#6507,.F.);
#8273=ORIENTED_EDGE('',*,*,#6506,.T.);
#8274=ORIENTED_EDGE('',*,*,#6508,.F.);
#8275=ORIENTED_EDGE('',*,*,#6481,.F.);
#8276=ORIENTED_EDGE('',*,*,#6396,.F.);
#8277=ORIENTED_EDGE('',*,*,#6393,.T.);
#8278=ORIENTED_EDGE('',*,*,#6389,.F.);
#8279=ORIENTED_EDGE('',*,*,#6412,.F.);
#8280=ORIENTED_EDGE('',*,*,#6442,.T.);
#8281=ORIENTED_EDGE('',*,*,#6443,.T.);
#8282=ORIENTED_EDGE('',*,*,#6418,.T.);
#8283=ORIENTED_EDGE('',*,*,#6422,.F.);
#8284=ORIENTED_EDGE('',*,*,#6425,.T.);
#8285=ORIENTED_EDGE('',*,*,#6447,.F.);
#8286=ORIENTED_EDGE('',*,*,#6483,.F.);
#8287=ORIENTED_EDGE('',*,*,#6486,.T.);
#8288=ORIENTED_EDGE('',*,*,#6489,.F.);
#8289=ORIENTED_EDGE('',*,*,#6492,.T.);
#8290=ORIENTED_EDGE('',*,*,#6495,.F.);
#8291=ORIENTED_EDGE('',*,*,#6498,.F.);
#8292=ORIENTED_EDGE('',*,*,#6501,.T.);
#8293=ORIENTED_EDGE('',*,*,#6504,.F.);
#8294=ORIENTED_EDGE('',*,*,#6507,.T.);
#8295=ORIENTED_EDGE('',*,*,#6480,.F.);
#8296=ORIENTED_EDGE('',*,*,#6477,.F.);
#8297=ORIENTED_EDGE('',*,*,#6474,.T.);
#8298=ORIENTED_EDGE('',*,*,#6471,.F.);
#8299=ORIENTED_EDGE('',*,*,#6468,.T.);
#8300=ORIENTED_EDGE('',*,*,#6465,.T.);
#8301=ORIENTED_EDGE('',*,*,#6462,.F.);
#8302=ORIENTED_EDGE('',*,*,#6459,.T.);
#8303=ORIENTED_EDGE('',*,*,#6456,.F.);
#8304=ORIENTED_EDGE('',*,*,#6453,.T.);
#8305=ORIENTED_EDGE('',*,*,#6448,.F.);
#8306=ORIENTED_EDGE('',*,*,#6452,.F.);
#8307=ORIENTED_EDGE('',*,*,#6428,.F.);
#8308=ORIENTED_EDGE('',*,*,#6432,.T.);
#8309=ORIENTED_EDGE('',*,*,#6435,.F.);
#8310=ORIENTED_EDGE('',*,*,#6438,.F.);
#8311=ORIENTED_EDGE('',*,*,#6415,.F.);
#8312=ORIENTED_EDGE('',*,*,#6409,.T.);
#8313=ORIENTED_EDGE('',*,*,#6406,.T.);
#8314=ORIENTED_EDGE('',*,*,#6403,.F.);
#8315=ORIENTED_EDGE('',*,*,#6399,.T.);
#8316=ORIENTED_EDGE('',*,*,#6450,.T.);
#8317=ORIENTED_EDGE('',*,*,#6455,.F.);
#8318=ORIENTED_EDGE('',*,*,#6458,.F.);
#8319=ORIENTED_EDGE('',*,*,#6461,.F.);
#8320=ORIENTED_EDGE('',*,*,#6464,.F.);
#8321=ORIENTED_EDGE('',*,*,#6467,.F.);
#8322=ORIENTED_EDGE('',*,*,#6470,.F.);
#8323=ORIENTED_EDGE('',*,*,#6473,.F.);
#8324=ORIENTED_EDGE('',*,*,#6476,.F.);
#8325=ORIENTED_EDGE('',*,*,#6479,.F.);
#8326=ORIENTED_EDGE('',*,*,#6482,.F.);
#8327=ORIENTED_EDGE('',*,*,#6508,.T.);
#8328=ORIENTED_EDGE('',*,*,#6505,.T.);
#8329=ORIENTED_EDGE('',*,*,#6502,.T.);
#8330=ORIENTED_EDGE('',*,*,#6499,.T.);
#8331=ORIENTED_EDGE('',*,*,#6496,.T.);
#8332=ORIENTED_EDGE('',*,*,#6493,.T.);
#8333=ORIENTED_EDGE('',*,*,#6490,.T.);
#8334=ORIENTED_EDGE('',*,*,#6487,.T.);
#8335=ORIENTED_EDGE('',*,*,#6484,.T.);
#8336=ORIENTED_EDGE('',*,*,#6445,.T.);
#8337=ORIENTED_EDGE('',*,*,#6426,.T.);
#8338=ORIENTED_EDGE('',*,*,#6423,.T.);
#8339=ORIENTED_EDGE('',*,*,#6420,.T.);
#8340=ORIENTED_EDGE('',*,*,#6444,.T.);
#8341=ORIENTED_EDGE('',*,*,#6440,.T.);
#8342=ORIENTED_EDGE('',*,*,#6413,.F.);
#8343=ORIENTED_EDGE('',*,*,#6391,.F.);
#8344=ORIENTED_EDGE('',*,*,#6395,.F.);
#8345=ORIENTED_EDGE('',*,*,#6398,.F.);
#8346=ORIENTED_EDGE('',*,*,#6401,.F.);
#8347=ORIENTED_EDGE('',*,*,#6405,.F.);
#8348=ORIENTED_EDGE('',*,*,#6408,.F.);
#8349=ORIENTED_EDGE('',*,*,#6411,.F.);
#8350=ORIENTED_EDGE('',*,*,#6417,.F.);
#8351=ORIENTED_EDGE('',*,*,#6439,.T.);
#8352=ORIENTED_EDGE('',*,*,#6436,.T.);
#8353=ORIENTED_EDGE('',*,*,#6433,.T.);
#8354=ORIENTED_EDGE('',*,*,#6430,.T.);
#8355=ORIENTED_EDGE('',*,*,#6451,.T.);
#10852=ADVANCED_FACE('',(#2976),#656,.F.);
#10853=ADVANCED_FACE('',(#2977),#2597,.F.);
#10854=ADVANCED_FACE('',(#2978),#657,.F.);
#10855=ADVANCED_FACE('',(#2979),#658,.F.);
#10856=ADVANCED_FACE('',(#2980),#2598,.T.);
#10857=ADVANCED_FACE('',(#2981),#659,.F.);
#10858=ADVANCED_FACE('',(#2982),#2599,.F.);
#10859=ADVANCED_FACE('',(#2983),#2600,.T.);
#10860=ADVANCED_FACE('',(#2984),#660,.T.);
#10861=ADVANCED_FACE('',(#2985),#661,.T.);
#10862=ADVANCED_FACE('',(#2986),#2601,.F.);
#10863=ADVANCED_FACE('',(#2987),#662,.T.);
#10864=ADVANCED_FACE('',(#2988),#663,.T.);
#10865=ADVANCED_FACE('',(#2989),#2602,.T.);
#10866=ADVANCED_FACE('',(#2990),#664,.T.);
#10867=ADVANCED_FACE('',(#2991),#2603,.F.);
#10868=ADVANCED_FACE('',(#2992),#665,.T.);
#10869=ADVANCED_FACE('',(#2993),#2604,.T.);
#10870=ADVANCED_FACE('',(#2994),#666,.T.);
#10871=ADVANCED_FACE('',(#2995),#667,.T.);
#10872=ADVANCED_FACE('',(#2996),#668,.T.);
#10873=ADVANCED_FACE('',(#2997),#2605,.F.);
#10874=ADVANCED_FACE('',(#2998),#669,.F.);
#10875=ADVANCED_FACE('',(#2999),#2606,.F.);
#10876=ADVANCED_FACE('',(#3000),#670,.F.);
#10877=ADVANCED_FACE('',(#3001),#671,.F.);
#10878=ADVANCED_FACE('',(#3002),#672,.F.);
#10879=ADVANCED_FACE('',(#3003),#2607,.T.);
#10880=ADVANCED_FACE('',(#3004),#673,.F.);
#10881=ADVANCED_FACE('',(#3005),#2608,.T.);
#10882=ADVANCED_FACE('',(#3006),#674,.T.);
#10883=ADVANCED_FACE('',(#3007),#2609,.F.);
#10884=ADVANCED_FACE('',(#3008),#675,.T.);
#10885=ADVANCED_FACE('',(#3009),#2610,.F.);
#10886=ADVANCED_FACE('',(#3010),#676,.T.);
#10887=ADVANCED_FACE('',(#3011),#677,.T.);
#10888=ADVANCED_FACE('',(#3012),#678,.T.);
#10889=ADVANCED_FACE('',(#3013),#2611,.T.);
#10890=ADVANCED_FACE('',(#3014),#679,.T.);
#10891=ADVANCED_FACE('',(#3015),#2612,.T.);
#10892=ADVANCED_FACE('',(#3016,#185),#680,.T.);
#10893=ADVANCED_FACE('',(#3017,#186),#681,.F.);
#11318=CLOSED_SHELL('',(#10852,#10853,#10854,#10855,#10856,#10857,#10858,
#10859,#10860,#10861,#10862,#10863,#10864,#10865,#10866,#10867,#10868,#10869,
#10870,#10871,#10872,#10873,#10874,#10875,#10876,#10877,#10878,#10879,#10880,
#10881,#10882,#10883,#10884,#10885,#10886,#10887,#10888,#10889,#10890,#10891,
#10892,#10893));
#11684=AXIS2_PLACEMENT_3D('',#16498,#13220,#13221);
#11685=AXIS2_PLACEMENT_3D('',#16499,#13222,#13223);
#11686=AXIS2_PLACEMENT_3D('',#16508,#13228,#13229);
#11687=AXIS2_PLACEMENT_3D('',#16510,#13230,#13231);
#11688=AXIS2_PLACEMENT_3D('',#16513,#13233,#13234);
#11689=AXIS2_PLACEMENT_3D('',#16514,#13235,#13236);
#11690=AXIS2_PLACEMENT_3D('',#16520,#13240,#13241);
#11691=AXIS2_PLACEMENT_3D('',#16529,#13246,#13247);
#11692=AXIS2_PLACEMENT_3D('',#16531,#13248,#13249);
#11693=AXIS2_PLACEMENT_3D('',#16534,#13251,#13252);
#11694=AXIS2_PLACEMENT_3D('',#16535,#13253,#13254);
#11695=AXIS2_PLACEMENT_3D('',#16541,#13258,#13259);
#11696=AXIS2_PLACEMENT_3D('',#16543,#13260,#13261);
#11697=AXIS2_PLACEMENT_3D('',#16546,#13263,#13264);
#11698=AXIS2_PLACEMENT_3D('',#16547,#13265,#13266);
#11699=AXIS2_PLACEMENT_3D('',#16549,#13267,#13268);
#11700=AXIS2_PLACEMENT_3D('',#16551,#13269,#13270);
#11701=AXIS2_PLACEMENT_3D('',#16553,#13272,#13273);
#11702=AXIS2_PLACEMENT_3D('',#16559,#13277,#13278);
#11703=AXIS2_PLACEMENT_3D('',#16568,#13283,#13284);
#11704=AXIS2_PLACEMENT_3D('',#16570,#13285,#13286);
#11705=AXIS2_PLACEMENT_3D('',#16572,#13287,#13288);
#11706=AXIS2_PLACEMENT_3D('',#16574,#13290,#13291);
#11707=AXIS2_PLACEMENT_3D('',#16580,#13295,#13296);
#11708=AXIS2_PLACEMENT_3D('',#16589,#13301,#13302);
#11709=AXIS2_PLACEMENT_3D('',#16591,#13303,#13304);
#11710=AXIS2_PLACEMENT_3D('',#16593,#13305,#13306);
#11711=AXIS2_PLACEMENT_3D('',#16595,#13308,#13309);
#11712=AXIS2_PLACEMENT_3D('',#16601,#13313,#13314);
#11713=AXIS2_PLACEMENT_3D('',#16602,#13315,#13316);
#11714=AXIS2_PLACEMENT_3D('',#16603,#13317,#13318);
#11715=AXIS2_PLACEMENT_3D('',#16604,#13319,#13320);
#11716=AXIS2_PLACEMENT_3D('',#16610,#13324,#13325);
#11717=AXIS2_PLACEMENT_3D('',#16611,#13326,#13327);
#11718=AXIS2_PLACEMENT_3D('',#16612,#13328,#13329);
#11719=AXIS2_PLACEMENT_3D('',#16613,#13330,#13331);
#11720=AXIS2_PLACEMENT_3D('',#16619,#13335,#13336);
#11721=AXIS2_PLACEMENT_3D('',#16625,#13340,#13341);
#11722=AXIS2_PLACEMENT_3D('',#16628,#13344,#13345);
#11723=AXIS2_PLACEMENT_3D('',#16630,#13346,#13347);
#11724=AXIS2_PLACEMENT_3D('',#16633,#13349,#13350);
#11725=AXIS2_PLACEMENT_3D('',#16634,#13351,#13352);
#11726=AXIS2_PLACEMENT_3D('',#16640,#13356,#13357);
#11727=AXIS2_PLACEMENT_3D('',#16642,#13358,#13359);
#11728=AXIS2_PLACEMENT_3D('',#16645,#13361,#13362);
#11729=AXIS2_PLACEMENT_3D('',#16646,#13363,#13364);
#11730=AXIS2_PLACEMENT_3D('',#16652,#13368,#13369);
#11731=AXIS2_PLACEMENT_3D('',#16658,#13373,#13374);
#11732=AXIS2_PLACEMENT_3D('',#16664,#13378,#13379);
#11733=AXIS2_PLACEMENT_3D('',#16666,#13380,#13381);
#11734=AXIS2_PLACEMENT_3D('',#16669,#13383,#13384);
#11735=AXIS2_PLACEMENT_3D('',#16670,#13385,#13386);
#11736=AXIS2_PLACEMENT_3D('',#16676,#13390,#13391);
#11737=AXIS2_PLACEMENT_3D('',#16678,#13392,#13393);
#11738=AXIS2_PLACEMENT_3D('',#16681,#13395,#13396);
#11739=AXIS2_PLACEMENT_3D('',#16682,#13397,#13398);
#11740=AXIS2_PLACEMENT_3D('',#16688,#13402,#13403);
#11741=AXIS2_PLACEMENT_3D('',#16690,#13404,#13405);
#11742=AXIS2_PLACEMENT_3D('',#16692,#13406,#13407);
#11743=AXIS2_PLACEMENT_3D('',#16694,#13409,#13410);
#11744=AXIS2_PLACEMENT_3D('',#16700,#13414,#13415);
#11745=AXIS2_PLACEMENT_3D('',#16702,#13416,#13417);
#11746=AXIS2_PLACEMENT_3D('',#16704,#13418,#13419);
#11747=AXIS2_PLACEMENT_3D('',#16706,#13421,#13422);
#11748=AXIS2_PLACEMENT_3D('',#16712,#13426,#13427);
#11749=AXIS2_PLACEMENT_3D('',#16718,#13431,#13432);
#11750=AXIS2_PLACEMENT_3D('',#16724,#13436,#13437);
#11751=AXIS2_PLACEMENT_3D('',#16726,#13438,#13439);
#11752=AXIS2_PLACEMENT_3D('',#16728,#13440,#13441);
#11753=AXIS2_PLACEMENT_3D('',#16730,#13443,#13444);
#11754=AXIS2_PLACEMENT_3D('',#16736,#13448,#13449);
#11755=AXIS2_PLACEMENT_3D('',#16737,#13450,#13451);
#11756=AXIS2_PLACEMENT_3D('',#16738,#13452,#13453);
#11757=AXIS2_PLACEMENT_3D('',#16739,#13454,#13455);
#11758=AXIS2_PLACEMENT_3D('',#16740,#13456,#13457);
#13220=DIRECTION('axis',(0.,0.,1.));
#13221=DIRECTION('refdir',(1.,0.,0.));
#13222=DIRECTION('center_axis',(0.,-0.984725314960397,0.174115059877505));
#13223=DIRECTION('ref_axis',(0.,0.174115059877505,0.984725314960397));
#13224=DIRECTION('',(0.,-0.174115059877505,-0.984725314960397));
#13225=DIRECTION('',(-1.,0.,0.));
#13226=DIRECTION('',(0.,0.174115059877505,0.984725314960397));
#13227=DIRECTION('',(-1.,0.,0.));
#13228=DIRECTION('center_axis',(1.,0.,0.));
#13229=DIRECTION('ref_axis',(0.,-0.821913269381079,-0.569612655771715));
#13230=DIRECTION('center_axis',(-1.,0.,0.));
#13231=DIRECTION('ref_axis',(0.,-0.821913269381079,-0.569612655771715));
#13232=DIRECTION('',(-1.,0.,0.));
#13233=DIRECTION('center_axis',(-1.,0.,0.));
#13234=DIRECTION('ref_axis',(0.,-0.821913269381079,-0.569612655771715));
#13235=DIRECTION('center_axis',(0.,-0.821913269381085,-0.569612655771705));
#13236=DIRECTION('ref_axis',(0.,-0.569612655771705,0.821913269381085));
#13237=DIRECTION('',(0.,0.569612655771705,-0.821913269381085));
#13238=DIRECTION('',(1.,0.,0.));
#13239=DIRECTION('',(0.,-0.569612655771705,0.821913269381085));
#13240=DIRECTION('center_axis',(0.,0.821913269381085,0.569612655771706));
#13241=DIRECTION('ref_axis',(0.,0.569612655771706,-0.821913269381085));
#13242=DIRECTION('',(0.,0.569612655771706,-0.821913269381085));
#13243=DIRECTION('',(-1.,0.,0.));
#13244=DIRECTION('',(0.,0.569612655771706,-0.821913269381085));
#13245=DIRECTION('',(-1.,0.,0.));
#13246=DIRECTION('center_axis',(1.,0.,0.));
#13247=DIRECTION('ref_axis',(0.,-0.821913269381079,-0.569612655771714));
#13248=DIRECTION('center_axis',(-1.,0.,0.));
#13249=DIRECTION('ref_axis',(0.,-0.821913269381079,-0.569612655771714));
#13250=DIRECTION('',(-1.,0.,0.));
#13251=DIRECTION('center_axis',(1.,0.,0.));
#13252=DIRECTION('ref_axis',(0.,-0.821913269381079,-0.569612655771714));
#13253=DIRECTION('center_axis',(0.,0.984725314960397,-0.174115059877505));
#13254=DIRECTION('ref_axis',(0.,-0.174115059877505,-0.984725314960397));
#13255=DIRECTION('',(0.,-0.174115059877505,-0.984725314960397));
#13256=DIRECTION('',(-1.,0.,0.));
#13257=DIRECTION('',(0.,-0.174115059877505,-0.984725314960397));
#13258=DIRECTION('center_axis',(1.,0.,0.));
#13259=DIRECTION('ref_axis',(0.,8.88178419700113E-15,1.));
#13260=DIRECTION('center_axis',(-1.,0.,0.));
#13261=DIRECTION('ref_axis',(0.,8.88178419700113E-15,1.));
#13262=DIRECTION('',(-1.,0.,0.));
#13263=DIRECTION('center_axis',(-1.,0.,0.));
#13264=DIRECTION('ref_axis',(0.,8.88178419700113E-15,1.));
#13265=DIRECTION('center_axis',(1.,0.,0.));
#13266=DIRECTION('ref_axis',(0.,0.,1.));
#13267=DIRECTION('center_axis',(-1.,0.,0.));
#13268=DIRECTION('ref_axis',(0.,0.,1.));
#13269=DIRECTION('center_axis',(1.,0.,0.));
#13270=DIRECTION('ref_axis',(0.,0.,1.));
#13271=DIRECTION('',(-1.,0.,0.));
#13272=DIRECTION('center_axis',(0.,-6.91402766832813E-16,-1.));
#13273=DIRECTION('ref_axis',(0.,-1.,6.91402766832813E-16));
#13274=DIRECTION('',(0.,-1.,6.91402766832813E-16));
#13275=DIRECTION('',(-1.,0.,0.));
#13276=DIRECTION('',(0.,1.,6.91402766832813E-16));
#13277=DIRECTION('center_axis',(0.,-0.984725314960397,-0.174115059877505));
#13278=DIRECTION('ref_axis',(0.,-0.174115059877505,0.984725314960397));
#13279=DIRECTION('',(0.,0.174115059877505,-0.984725314960397));
#13280=DIRECTION('',(-1.,0.,0.));
#13281=DIRECTION('',(0.,-0.174115059877505,0.984725314960397));
#13282=DIRECTION('',(-1.,0.,0.));
#13283=DIRECTION('center_axis',(-1.,0.,0.));
#13284=DIRECTION('ref_axis',(0.,0.821913269381079,-0.569612655771715));
#13285=DIRECTION('center_axis',(1.,0.,0.));
#13286=DIRECTION('ref_axis',(0.,0.821913269381079,-0.569612655771715));
#13287=DIRECTION('center_axis',(1.,0.,0.));
#13288=DIRECTION('ref_axis',(0.,0.821913269381079,-0.569612655771715));
#13289=DIRECTION('',(-1.,0.,0.));
#13290=DIRECTION('center_axis',(0.,-0.821913269381085,0.569612655771705));
#13291=DIRECTION('ref_axis',(0.,0.569612655771705,0.821913269381085));
#13292=DIRECTION('',(0.,-0.569612655771705,-0.821913269381085));
#13293=DIRECTION('',(0.,0.569612655771705,0.821913269381085));
#13294=DIRECTION('',(-1.,0.,0.));
#13295=DIRECTION('center_axis',(0.,0.821913269381085,-0.569612655771706));
#13296=DIRECTION('ref_axis',(0.,-0.569612655771706,-0.821913269381085));
#13297=DIRECTION('',(0.,-0.569612655771706,-0.821913269381085));
#13298=DIRECTION('',(1.,0.,0.));
#13299=DIRECTION('',(0.,-0.569612655771706,-0.821913269381085));
#13300=DIRECTION('',(-1.,0.,0.));
#13301=DIRECTION('center_axis',(-1.,0.,0.));
#13302=DIRECTION('ref_axis',(0.,0.821913269381079,-0.569612655771714));
#13303=DIRECTION('center_axis',(1.,0.,0.));
#13304=DIRECTION('ref_axis',(0.,0.821913269381079,-0.569612655771714));
#13305=DIRECTION('center_axis',(-1.,0.,0.));
#13306=DIRECTION('ref_axis',(0.,0.821913269381079,-0.569612655771714));
#13307=DIRECTION('',(-1.,0.,0.));
#13308=DIRECTION('center_axis',(0.,0.984725314960397,0.174115059877505));
#13309=DIRECTION('ref_axis',(0.,0.174115059877505,-0.984725314960397));
#13310=DIRECTION('',(0.,0.174115059877505,-0.984725314960397));
#13311=DIRECTION('',(0.,0.174115059877505,-0.984725314960397));
#13312=DIRECTION('',(-1.,0.,0.));
#13313=DIRECTION('center_axis',(-1.,0.,0.));
#13314=DIRECTION('ref_axis',(0.,-8.88178419700113E-15,1.));
#13315=DIRECTION('center_axis',(1.,0.,0.));
#13316=DIRECTION('ref_axis',(0.,-8.88178419700113E-15,1.));
#13317=DIRECTION('center_axis',(1.,0.,0.));
#13318=DIRECTION('ref_axis',(0.,-8.88178419700113E-15,1.));
#13319=DIRECTION('center_axis',(0.,0.,1.));
#13320=DIRECTION('ref_axis',(0.,1.,0.));
#13321=DIRECTION('',(0.,1.,0.));
#13322=DIRECTION('',(-1.,0.,0.));
#13323=DIRECTION('',(0.,-1.,0.));
#13324=DIRECTION('center_axis',(-1.,0.,0.));
#13325=DIRECTION('ref_axis',(0.,0.,1.));
#13326=DIRECTION('center_axis',(1.,0.,0.));
#13327=DIRECTION('ref_axis',(0.,0.,1.));
#13328=DIRECTION('center_axis',(-1.,0.,0.));
#13329=DIRECTION('ref_axis',(0.,0.,1.));
#13330=DIRECTION('center_axis',(0.,0.,1.));
#13331=DIRECTION('ref_axis',(0.,1.,0.));
#13332=DIRECTION('',(0.,1.,0.));
#13333=DIRECTION('',(-1.,0.,0.));
#13334=DIRECTION('',(0.,1.,0.));
#13335=DIRECTION('center_axis',(0.,0.,1.));
#13336=DIRECTION('ref_axis',(0.,1.,0.));
#13337=DIRECTION('',(0.,1.,0.));
#13338=DIRECTION('',(-1.,0.,0.));
#13339=DIRECTION('',(0.,1.,0.));
#13340=DIRECTION('center_axis',(0.,0.,1.));
#13341=DIRECTION('ref_axis',(0.,1.,0.));
#13342=DIRECTION('',(0.,1.,0.));
#13343=DIRECTION('',(0.,1.,0.));
#13344=DIRECTION('center_axis',(1.,0.,0.));
#13345=DIRECTION('ref_axis',(0.,0.707106781186555,-0.70710678118654));
#13346=DIRECTION('center_axis',(-1.,0.,0.));
#13347=DIRECTION('ref_axis',(0.,0.707106781186555,-0.70710678118654));
#13348=DIRECTION('',(-1.,0.,0.));
#13349=DIRECTION('center_axis',(-1.,0.,0.));
#13350=DIRECTION('ref_axis',(0.,0.707106781186555,-0.70710678118654));
#13351=DIRECTION('center_axis',(0.,0.707106781186548,-0.707106781186548));
#13352=DIRECTION('ref_axis',(0.,-0.707106781186548,-0.707106781186548));
#13353=DIRECTION('',(0.,0.707106781186547,0.707106781186547));
#13354=DIRECTION('',(-1.,0.,0.));
#13355=DIRECTION('',(0.,-0.707106781186547,-0.707106781186547));
#13356=DIRECTION('center_axis',(1.,0.,0.));
#13357=DIRECTION('ref_axis',(0.,0.98480775301221,-0.17364817766692));
#13358=DIRECTION('center_axis',(-1.,0.,0.));
#13359=DIRECTION('ref_axis',(0.,0.98480775301221,-0.17364817766692));
#13360=DIRECTION('',(-1.,0.,0.));
#13361=DIRECTION('center_axis',(-1.,0.,0.));
#13362=DIRECTION('ref_axis',(0.,0.98480775301221,-0.17364817766692));
#13363=DIRECTION('center_axis',(0.,0.984807753012208,-0.173648177666932));
#13364=DIRECTION('ref_axis',(0.,-0.173648177666932,-0.984807753012208));
#13365=DIRECTION('',(0.,0.173648177666932,0.984807753012208));
#13366=DIRECTION('',(-1.,0.,0.));
#13367=DIRECTION('',(0.,-0.173648177666932,-0.984807753012208));
#13368=DIRECTION('center_axis',(0.,0.,-1.));
#13369=DIRECTION('ref_axis',(0.,-1.,0.));
#13370=DIRECTION('',(0.,-1.,0.));
#13371=DIRECTION('',(-1.,0.,0.));
#13372=DIRECTION('',(0.,-1.,0.));
#13373=DIRECTION('center_axis',(0.,-0.984807753012208,0.173648177666932));
#13374=DIRECTION('ref_axis',(0.,0.173648177666932,0.984807753012208));
#13375=DIRECTION('',(0.,0.173648177666932,0.984807753012208));
#13376=DIRECTION('',(-1.,0.,0.));
#13377=DIRECTION('',(0.,0.173648177666932,0.984807753012208));
#13378=DIRECTION('center_axis',(1.,0.,0.));
#13379=DIRECTION('ref_axis',(0.,0.984807753012209,-0.173648177666926));
#13380=DIRECTION('center_axis',(-1.,0.,0.));
#13381=DIRECTION('ref_axis',(0.,0.984807753012209,-0.173648177666926));
#13382=DIRECTION('',(-1.,0.,0.));
#13383=DIRECTION('center_axis',(1.,0.,0.));
#13384=DIRECTION('ref_axis',(0.,0.984807753012209,-0.173648177666926));
#13385=DIRECTION('center_axis',(0.,-0.707106781186547,0.707106781186548));
#13386=DIRECTION('ref_axis',(0.,0.707106781186548,0.707106781186547));
#13387=DIRECTION('',(0.,0.707106781186548,0.707106781186547));
#13388=DIRECTION('',(-1.,0.,0.));
#13389=DIRECTION('',(0.,0.707106781186548,0.707106781186547));
#13390=DIRECTION('center_axis',(1.,0.,0.));
#13391=DIRECTION('ref_axis',(0.,0.707106781186551,-0.707106781186544));
#13392=DIRECTION('center_axis',(-1.,0.,0.));
#13393=DIRECTION('ref_axis',(0.,0.707106781186551,-0.707106781186544));
#13394=DIRECTION('',(-1.,0.,0.));
#13395=DIRECTION('center_axis',(1.,0.,0.));
#13396=DIRECTION('ref_axis',(0.,0.707106781186551,-0.707106781186544));
#13397=DIRECTION('center_axis',(0.,0.,-1.));
#13398=DIRECTION('ref_axis',(0.,-1.,0.));
#13399=DIRECTION('',(0.,-1.,0.));
#13400=DIRECTION('',(-1.,0.,0.));
#13401=DIRECTION('',(0.,1.,0.));
#13402=DIRECTION('center_axis',(-1.,0.,0.));
#13403=DIRECTION('ref_axis',(0.,-0.707106781186555,-0.70710678118654));
#13404=DIRECTION('center_axis',(1.,0.,0.));
#13405=DIRECTION('ref_axis',(0.,-0.707106781186555,-0.70710678118654));
#13406=DIRECTION('center_axis',(1.,0.,0.));
#13407=DIRECTION('ref_axis',(0.,-0.707106781186555,-0.70710678118654));
#13408=DIRECTION('',(-1.,0.,0.));
#13409=DIRECTION('center_axis',(0.,0.707106781186548,0.707106781186548));
#13410=DIRECTION('ref_axis',(0.,0.707106781186548,-0.707106781186548));
#13411=DIRECTION('',(0.,-0.707106781186547,0.707106781186547));
#13412=DIRECTION('',(0.,0.707106781186547,-0.707106781186547));
#13413=DIRECTION('',(-1.,0.,0.));
#13414=DIRECTION('center_axis',(-1.,0.,0.));
#13415=DIRECTION('ref_axis',(0.,-0.98480775301221,-0.17364817766692));
#13416=DIRECTION('center_axis',(1.,0.,0.));
#13417=DIRECTION('ref_axis',(0.,-0.98480775301221,-0.17364817766692));
#13418=DIRECTION('center_axis',(1.,0.,0.));
#13419=DIRECTION('ref_axis',(0.,-0.98480775301221,-0.17364817766692));
#13420=DIRECTION('',(-1.,0.,0.));
#13421=DIRECTION('center_axis',(0.,0.984807753012208,0.173648177666932));
#13422=DIRECTION('ref_axis',(0.,0.173648177666932,-0.984807753012208));
#13423=DIRECTION('',(0.,-0.173648177666932,0.984807753012208));
#13424=DIRECTION('',(0.,0.173648177666932,-0.984807753012208));
#13425=DIRECTION('',(-1.,0.,0.));
#13426=DIRECTION('center_axis',(0.,0.,1.));
#13427=DIRECTION('ref_axis',(0.,1.,0.));
#13428=DIRECTION('',(0.,1.,0.));
#13429=DIRECTION('',(0.,1.,0.));
#13430=DIRECTION('',(-1.,0.,0.));
#13431=DIRECTION('center_axis',(0.,-0.984807753012208,-0.173648177666932));
#13432=DIRECTION('ref_axis',(0.,-0.173648177666932,0.984807753012208));
#13433=DIRECTION('',(0.,-0.173648177666932,0.984807753012208));
#13434=DIRECTION('',(0.,-0.173648177666932,0.984807753012208));
#13435=DIRECTION('',(-1.,0.,0.));
#13436=DIRECTION('center_axis',(-1.,0.,0.));
#13437=DIRECTION('ref_axis',(0.,-0.984807753012209,-0.173648177666926));
#13438=DIRECTION('center_axis',(1.,0.,0.));
#13439=DIRECTION('ref_axis',(0.,-0.984807753012209,-0.173648177666926));
#13440=DIRECTION('center_axis',(-1.,0.,0.));
#13441=DIRECTION('ref_axis',(0.,-0.984807753012209,-0.173648177666926));
#13442=DIRECTION('',(-1.,0.,0.));
#13443=DIRECTION('center_axis',(0.,-0.707106781186547,-0.707106781186548));
#13444=DIRECTION('ref_axis',(0.,-0.707106781186548,0.707106781186547));
#13445=DIRECTION('',(0.,-0.707106781186548,0.707106781186547));
#13446=DIRECTION('',(0.,-0.707106781186548,0.707106781186547));
#13447=DIRECTION('',(-1.,0.,0.));
#13448=DIRECTION('center_axis',(-1.,0.,0.));
#13449=DIRECTION('ref_axis',(0.,-0.707106781186551,-0.707106781186544));
#13450=DIRECTION('center_axis',(1.,0.,0.));
#13451=DIRECTION('ref_axis',(0.,-0.707106781186551,-0.707106781186544));
#13452=DIRECTION('center_axis',(-1.,0.,0.));
#13453=DIRECTION('ref_axis',(0.,-0.707106781186551,-0.707106781186544));
#13454=DIRECTION('center_axis',(1.,0.,0.));
#13455=DIRECTION('ref_axis',(0.,1.,0.));
#13456=DIRECTION('center_axis',(1.,0.,0.));
#13457=DIRECTION('ref_axis',(0.,1.,0.));
#16498=CARTESIAN_POINT('',(0.,0.,0.));
#16499=CARTESIAN_POINT('Origin',(384.,29.4811336906747,16.5456750096756));
#16500=CARTESIAN_POINT('',(384.,29.8952421751416,18.8877073880428));
#16501=CARTESIAN_POINT('',(384.,29.4811336906747,16.5456750096756));
#16502=CARTESIAN_POINT('',(384.,29.8952421751416,18.8877073880428));
#16503=CARTESIAN_POINT('',(47.9470000000001,29.4811336906747,16.5456750096756));
#16504=CARTESIAN_POINT('',(384.,29.4811336906747,16.5456750096756));
#16505=CARTESIAN_POINT('',(47.9470000000001,29.8952421751416,18.8877073880428));
#16506=CARTESIAN_POINT('',(47.9470000000001,29.8952421751416,18.8877073880428));
#16507=CARTESIAN_POINT('',(384.,29.8952421751416,18.8877073880428));
#16508=CARTESIAN_POINT('Origin',(384.,30.465859005635,16.3715599497981));
#16509=CARTESIAN_POINT('',(384.,29.643945736254,15.8019472940264));
#16510=CARTESIAN_POINT('Origin',(384.,30.465859005635,16.3715599497981));
#16511=CARTESIAN_POINT('',(47.9470000000001,29.643945736254,15.8019472940264));
#16512=CARTESIAN_POINT('',(384.,29.643945736254,15.8019472940264));
#16513=CARTESIAN_POINT('Origin',(47.9470000000001,30.465859005635,16.3715599497981));
#16514=CARTESIAN_POINT('Origin',(384.,31.5857864376269,13.));
#16515=CARTESIAN_POINT('',(384.,31.5857864376269,13.));
#16516=CARTESIAN_POINT('',(384.,29.643945736254,15.8019472940264));
#16517=CARTESIAN_POINT('',(47.9470000000001,31.5857864376269,13.));
#16518=CARTESIAN_POINT('',(384.,31.5857864376269,13.));
#16519=CARTESIAN_POINT('',(47.9470000000001,29.643945736254,15.8019472940264));
#16520=CARTESIAN_POINT('Origin',(384.,28.8220324668729,15.2323346382546));
#16521=CARTESIAN_POINT('',(384.,28.8220324668729,15.2323346382546));
#16522=CARTESIAN_POINT('',(384.,30.369113052182,13.));
#16523=CARTESIAN_POINT('',(384.,28.8220324668729,15.2323346382546));
#16524=CARTESIAN_POINT('',(47.9470000000001,28.8220324668729,15.2323346382546));
#16525=CARTESIAN_POINT('',(384.,28.8220324668729,15.2323346382546));
#16526=CARTESIAN_POINT('',(47.9470000000001,30.369113052182,13.));
#16527=CARTESIAN_POINT('',(47.9470000000001,28.8220324668729,15.2323346382546));
#16528=CARTESIAN_POINT('',(384.,30.369113052182,13.));
#16529=CARTESIAN_POINT('Origin',(384.,30.465859005635,16.3715599497981));
#16530=CARTESIAN_POINT('',(384.,28.4964083757143,16.7197900695531));
#16531=CARTESIAN_POINT('Origin',(384.,30.465859005635,16.3715599497981));
#16532=CARTESIAN_POINT('',(47.9470000000001,28.4964083757143,16.7197900695531));
#16533=CARTESIAN_POINT('',(384.,28.4964083757143,16.7197900695531));
#16534=CARTESIAN_POINT('Origin',(47.9470000000001,30.465859005635,16.3715599497981));
#16535=CARTESIAN_POINT('Origin',(384.,28.7029146884407,17.8877073880428));
#16536=CARTESIAN_POINT('',(384.,28.7029146884407,17.8877073880428));
#16537=CARTESIAN_POINT('',(384.,28.7029146884407,17.8877073880428));
#16538=CARTESIAN_POINT('',(47.9470000000001,28.7029146884407,17.8877073880428));
#16539=CARTESIAN_POINT('',(384.,28.7029146884407,17.8877073880428));
#16540=CARTESIAN_POINT('',(47.9470000000001,28.7029146884407,17.8877073880428));
#16541=CARTESIAN_POINT('Origin',(384.,28.2105520309605,17.9747649179816));
#16542=CARTESIAN_POINT('',(384.,28.2105520309605,18.4747649179816));
#16543=CARTESIAN_POINT('Origin',(384.,28.2105520309605,17.9747649179816));
#16544=CARTESIAN_POINT('',(47.9470000000001,28.2105520309605,18.4747649179816));
#16545=CARTESIAN_POINT('',(384.,28.2105520309605,18.4747649179816));
#16546=CARTESIAN_POINT('Origin',(47.9470000000001,28.2105520309605,17.9747649179816));
#16547=CARTESIAN_POINT('Origin',(384.,29.4028795176614,18.9747649179816));
#16548=CARTESIAN_POINT('',(384.,29.4028795176614,19.4747649179816));
#16549=CARTESIAN_POINT('Origin',(384.,29.4028795176614,18.9747649179816));
#16550=CARTESIAN_POINT('',(47.9470000000001,29.4028795176614,19.4747649179816));
#16551=CARTESIAN_POINT('Origin',(47.9470000000001,29.4028795176614,18.9747649179816));
#16552=CARTESIAN_POINT('',(384.,29.4028795176614,19.4747649179816));
#16553=CARTESIAN_POINT('Origin',(384.,25.0009567389882,18.4747649179816));
#16554=CARTESIAN_POINT('',(384.,21.7894479690395,18.4747649179816));
#16555=CARTESIAN_POINT('',(384.,25.0009567389882,18.4747649179816));
#16556=CARTESIAN_POINT('',(47.9470000000001,21.7894479690395,18.4747649179816));
#16557=CARTESIAN_POINT('',(384.,21.7894479690395,18.4747649179816));
#16558=CARTESIAN_POINT('',(47.9470000000001,24.9990432610118,18.4747649179816));
#16559=CARTESIAN_POINT('Origin',(384.,20.5188663093253,16.5456750096756));
#16560=CARTESIAN_POINT('',(384.,20.1047578248584,18.8877073880428));
#16561=CARTESIAN_POINT('',(384.,20.5188663093253,16.5456750096756));
#16562=CARTESIAN_POINT('',(384.,20.1047578248584,18.8877073880428));
#16563=CARTESIAN_POINT('',(47.9470000000001,20.1047578248584,18.8877073880428));
#16564=CARTESIAN_POINT('',(384.,20.1047578248584,18.8877073880428));
#16565=CARTESIAN_POINT('',(47.9470000000001,20.5188663093253,16.5456750096756));
#16566=CARTESIAN_POINT('',(47.9470000000001,20.1047578248584,18.8877073880428));
#16567=CARTESIAN_POINT('',(384.,20.5188663093253,16.5456750096756));
#16568=CARTESIAN_POINT('Origin',(384.,19.534140994365,16.3715599497981));
#16569=CARTESIAN_POINT('',(384.,20.356054263746,15.8019472940264));
#16570=CARTESIAN_POINT('Origin',(384.,19.534140994365,16.3715599497981));
#16571=CARTESIAN_POINT('',(47.9470000000001,20.356054263746,15.8019472940264));
#16572=CARTESIAN_POINT('Origin',(47.9470000000001,19.534140994365,16.3715599497981));
#16573=CARTESIAN_POINT('',(384.,20.356054263746,15.8019472940264));
#16574=CARTESIAN_POINT('Origin',(384.,18.4142135623731,13.));
#16575=CARTESIAN_POINT('',(384.,18.4142135623731,13.));
#16576=CARTESIAN_POINT('',(384.,20.356054263746,15.8019472940264));
#16577=CARTESIAN_POINT('',(47.9470000000001,18.4142135623731,13.));
#16578=CARTESIAN_POINT('',(47.9470000000001,20.356054263746,15.8019472940264));
#16579=CARTESIAN_POINT('',(384.,18.4142135623731,13.));
#16580=CARTESIAN_POINT('Origin',(384.,21.1779675331271,15.2323346382546));
#16581=CARTESIAN_POINT('',(384.,21.1779675331271,15.2323346382546));
#16582=CARTESIAN_POINT('',(384.,19.630886947818,13.));
#16583=CARTESIAN_POINT('',(384.,21.1779675331271,15.2323346382546));
#16584=CARTESIAN_POINT('',(47.9470000000001,19.630886947818,13.));
#16585=CARTESIAN_POINT('',(384.,19.630886947818,13.));
#16586=CARTESIAN_POINT('',(47.9470000000001,21.1779675331271,15.2323346382546));
#16587=CARTESIAN_POINT('',(47.9470000000001,21.1779675331271,15.2323346382546));
#16588=CARTESIAN_POINT('',(384.,21.1779675331271,15.2323346382546));
#16589=CARTESIAN_POINT('Origin',(384.,19.534140994365,16.3715599497981));
#16590=CARTESIAN_POINT('',(384.,21.5035916242857,16.7197900695531));
#16591=CARTESIAN_POINT('Origin',(384.,19.534140994365,16.3715599497981));
#16592=CARTESIAN_POINT('',(47.9470000000001,21.5035916242857,16.7197900695531));
#16593=CARTESIAN_POINT('Origin',(47.9470000000001,19.534140994365,16.3715599497981));
#16594=CARTESIAN_POINT('',(384.,21.5035916242857,16.7197900695531));
#16595=CARTESIAN_POINT('Origin',(384.,21.2970853115593,17.8877073880428));
#16596=CARTESIAN_POINT('',(384.,21.2970853115593,17.8877073880428));
#16597=CARTESIAN_POINT('',(384.,21.2970853115593,17.8877073880428));
#16598=CARTESIAN_POINT('',(47.9470000000001,21.2970853115593,17.8877073880428));
#16599=CARTESIAN_POINT('',(47.9470000000001,21.2970853115593,17.8877073880428));
#16600=CARTESIAN_POINT('',(384.,21.2970853115593,17.8877073880428));
#16601=CARTESIAN_POINT('Origin',(384.,21.7894479690395,17.9747649179816));
#16602=CARTESIAN_POINT('Origin',(384.,21.7894479690395,17.9747649179816));
#16603=CARTESIAN_POINT('Origin',(47.9470000000001,21.7894479690395,17.9747649179816));
#16604=CARTESIAN_POINT('Origin',(384.,20.5971204823386,19.4747649179816));
#16605=CARTESIAN_POINT('',(47.9470000000001,20.5971204823386,19.4747649179816));
#16606=CARTESIAN_POINT('',(47.9470000000001,25.0009567389882,19.4747649179816));
#16607=CARTESIAN_POINT('',(384.,20.5971204823386,19.4747649179816));
#16608=CARTESIAN_POINT('',(384.,20.5971204823386,19.4747649179816));
#16609=CARTESIAN_POINT('',(384.,25.0009567389882,19.4747649179816));
#16610=CARTESIAN_POINT('Origin',(384.,20.5971204823386,18.9747649179816));
#16611=CARTESIAN_POINT('Origin',(384.,20.5971204823386,18.9747649179816));
#16612=CARTESIAN_POINT('Origin',(47.9470000000001,20.5971204823386,18.9747649179816));
#16613=CARTESIAN_POINT('Origin',(384.,15.8284271247462,13.));
#16614=CARTESIAN_POINT('',(47.9470000000001,15.8284271247462,13.));
#16615=CARTESIAN_POINT('',(47.9470000000001,21.,13.));
#16616=CARTESIAN_POINT('',(384.,15.8284271247462,13.));
#16617=CARTESIAN_POINT('',(384.,15.8284271247462,13.));
#16618=CARTESIAN_POINT('',(384.,21.,13.));
#16619=CARTESIAN_POINT('Origin',(384.,15.8284271247462,13.));
#16620=CARTESIAN_POINT('',(384.,34.1715728752538,13.));
#16621=CARTESIAN_POINT('',(384.,21.,13.));
#16622=CARTESIAN_POINT('',(47.9470000000001,34.1715728752538,13.));
#16623=CARTESIAN_POINT('',(384.,34.1715728752538,13.));
#16624=CARTESIAN_POINT('',(47.9470000000001,21.,13.));
#16625=CARTESIAN_POINT('Origin',(384.,15.8284271247462,13.));
#16626=CARTESIAN_POINT('',(47.9470000000001,21.,13.));
#16627=CARTESIAN_POINT('',(384.,21.,13.));
#16628=CARTESIAN_POINT('Origin',(384.,34.1715728752538,14.));
#16629=CARTESIAN_POINT('',(384.,34.8786796564404,13.2928932188135));
#16630=CARTESIAN_POINT('Origin',(384.,34.1715728752538,14.));
#16631=CARTESIAN_POINT('',(47.9470000000001,34.8786796564404,13.2928932188135));
#16632=CARTESIAN_POINT('',(384.,34.8786796564404,13.2928932188135));
#16633=CARTESIAN_POINT('Origin',(47.9470000000001,34.1715728752538,14.));
#16634=CARTESIAN_POINT('Origin',(384.,37.3825273013137,15.7967408636868));
#16635=CARTESIAN_POINT('',(384.,37.3825273013137,15.7967408636868));
#16636=CARTESIAN_POINT('',(384.,34.8786796564404,13.2928932188135));
#16637=CARTESIAN_POINT('',(47.9470000000001,37.3825273013137,15.7967408636868));
#16638=CARTESIAN_POINT('',(384.,37.3825273013137,15.7967408636868));
#16639=CARTESIAN_POINT('',(47.9470000000001,34.8786796564404,13.2928932188135));
#16640=CARTESIAN_POINT('Origin',(384.,36.6754205201272,16.5038476448733));
#16641=CARTESIAN_POINT('',(384.,37.6602282731394,16.3301994672064));
#16642=CARTESIAN_POINT('Origin',(384.,36.6754205201272,16.5038476448733));
#16643=CARTESIAN_POINT('',(47.9470000000001,37.6602282731394,16.3301994672064));
#16644=CARTESIAN_POINT('',(384.,37.6602282731394,16.3301994672064));
#16645=CARTESIAN_POINT('Origin',(47.9470000000001,36.6754205201272,16.5038476448733));
#16646=CARTESIAN_POINT('Origin',(384.,38.2147000047147,19.4747649179816));
#16647=CARTESIAN_POINT('',(384.,38.2147000047147,19.4747649179816));
#16648=CARTESIAN_POINT('',(384.,37.6602282731394,16.3301994672064));
#16649=CARTESIAN_POINT('',(47.9470000000001,38.2147000047147,19.4747649179816));
#16650=CARTESIAN_POINT('',(384.,38.2147000047147,19.4747649179816));
#16651=CARTESIAN_POINT('',(47.9470000000001,37.6602282731394,16.3301994672064));
#16652=CARTESIAN_POINT('Origin',(384.,39.2301266166005,19.4747649179816));
#16653=CARTESIAN_POINT('',(384.,39.2301266166005,19.4747649179816));
#16654=CARTESIAN_POINT('',(384.,39.2301266166005,19.4747649179816));
#16655=CARTESIAN_POINT('',(47.9470000000001,39.2301266166005,19.4747649179816));
#16656=CARTESIAN_POINT('',(384.,39.2301266166005,19.4747649179816));
#16657=CARTESIAN_POINT('',(47.9470000000001,39.2301266166005,19.4747649179816));
#16658=CARTESIAN_POINT('Origin',(384.,38.6450360261516,16.1565512895395));
#16659=CARTESIAN_POINT('',(384.,38.6450360261516,16.1565512895395));
#16660=CARTESIAN_POINT('',(384.,38.6450360261516,16.1565512895395));
#16661=CARTESIAN_POINT('',(47.9470000000001,38.6450360261516,16.1565512895395));
#16662=CARTESIAN_POINT('',(384.,38.6450360261516,16.1565512895395));
#16663=CARTESIAN_POINT('',(47.9470000000001,38.6450360261516,16.1565512895395));
#16664=CARTESIAN_POINT('Origin',(384.,36.6754205201272,16.5038476448733));
#16665=CARTESIAN_POINT('',(384.,38.0896340825003,15.0896340825003));
#16666=CARTESIAN_POINT('Origin',(384.,36.6754205201272,16.5038476448733));
#16667=CARTESIAN_POINT('',(47.9470000000001,38.0896340825003,15.0896340825003));
#16668=CARTESIAN_POINT('',(384.,38.0896340825003,15.0896340825003));
#16669=CARTESIAN_POINT('Origin',(47.9470000000001,36.6754205201272,16.5038476448733));
#16670=CARTESIAN_POINT('Origin',(384.,35.5857864376269,12.5857864376269));
#16671=CARTESIAN_POINT('',(384.,35.5857864376269,12.5857864376269));
#16672=CARTESIAN_POINT('',(384.,35.5857864376269,12.5857864376269));
#16673=CARTESIAN_POINT('',(47.9470000000001,35.5857864376269,12.5857864376269));
#16674=CARTESIAN_POINT('',(384.,35.5857864376269,12.5857864376269));
#16675=CARTESIAN_POINT('',(47.9470000000001,35.5857864376269,12.5857864376269));
#16676=CARTESIAN_POINT('Origin',(384.,34.1715728752538,14.));
#16677=CARTESIAN_POINT('',(384.,34.1715728752538,12.));
#16678=CARTESIAN_POINT('Origin',(384.,34.1715728752538,14.));
#16679=CARTESIAN_POINT('',(47.9470000000001,34.1715728752538,12.));
#16680=CARTESIAN_POINT('',(384.,34.1715728752538,12.));
#16681=CARTESIAN_POINT('Origin',(47.9470000000001,34.1715728752538,14.));
#16682=CARTESIAN_POINT('Origin',(384.,25.,12.));
#16683=CARTESIAN_POINT('',(384.,15.8284271247462,12.));
#16684=CARTESIAN_POINT('',(384.,25.,12.));
#16685=CARTESIAN_POINT('',(47.9470000000001,15.8284271247462,12.));
#16686=CARTESIAN_POINT('',(384.,15.8284271247462,12.));
#16687=CARTESIAN_POINT('',(47.9470000000001,25.,12.));
#16688=CARTESIAN_POINT('Origin',(384.,15.8284271247462,14.));
#16689=CARTESIAN_POINT('',(384.,15.1213203435596,13.2928932188135));
#16690=CARTESIAN_POINT('Origin',(384.,15.8284271247462,14.));
#16691=CARTESIAN_POINT('',(47.9470000000001,15.1213203435596,13.2928932188135));
#16692=CARTESIAN_POINT('Origin',(47.9470000000001,15.8284271247462,14.));
#16693=CARTESIAN_POINT('',(384.,15.1213203435596,13.2928932188135));
#16694=CARTESIAN_POINT('Origin',(384.,12.6174726986863,15.7967408636868));
#16695=CARTESIAN_POINT('',(384.,12.6174726986863,15.7967408636868));
#16696=CARTESIAN_POINT('',(384.,15.1213203435596,13.2928932188135));
#16697=CARTESIAN_POINT('',(47.9470000000001,12.6174726986863,15.7967408636868));
#16698=CARTESIAN_POINT('',(47.9470000000001,15.1213203435596,13.2928932188135));
#16699=CARTESIAN_POINT('',(384.,12.6174726986863,15.7967408636868));
#16700=CARTESIAN_POINT('Origin',(384.,13.3245794798728,16.5038476448733));
#16701=CARTESIAN_POINT('',(384.,12.3397717268606,16.3301994672064));
#16702=CARTESIAN_POINT('Origin',(384.,13.3245794798728,16.5038476448733));
#16703=CARTESIAN_POINT('',(47.9470000000001,12.3397717268606,16.3301994672064));
#16704=CARTESIAN_POINT('Origin',(47.9470000000001,13.3245794798728,16.5038476448733));
#16705=CARTESIAN_POINT('',(384.,12.3397717268606,16.3301994672064));
#16706=CARTESIAN_POINT('Origin',(384.,11.7852999952853,19.4747649179816));
#16707=CARTESIAN_POINT('',(384.,11.7852999952853,19.4747649179816));
#16708=CARTESIAN_POINT('',(384.,12.3397717268606,16.3301994672064));
#16709=CARTESIAN_POINT('',(47.9470000000001,11.7852999952853,19.4747649179816));
#16710=CARTESIAN_POINT('',(47.9470000000001,12.3397717268606,16.3301994672064));
#16711=CARTESIAN_POINT('',(384.,11.7852999952853,19.4747649179816));
#16712=CARTESIAN_POINT('Origin',(384.,10.7698733833995,19.4747649179816));
#16713=CARTESIAN_POINT('',(384.,10.7698733833995,19.4747649179816));
#16714=CARTESIAN_POINT('',(384.,10.7698733833995,19.4747649179816));
#16715=CARTESIAN_POINT('',(47.9470000000001,10.7698733833995,19.4747649179816));
#16716=CARTESIAN_POINT('',(47.9470000000001,10.7698733833995,19.4747649179816));
#16717=CARTESIAN_POINT('',(384.,10.7698733833995,19.4747649179816));
#16718=CARTESIAN_POINT('Origin',(384.,11.3549639738484,16.1565512895395));
#16719=CARTESIAN_POINT('',(384.,11.3549639738484,16.1565512895395));
#16720=CARTESIAN_POINT('',(384.,11.3549639738484,16.1565512895395));
#16721=CARTESIAN_POINT('',(47.9470000000001,11.3549639738484,16.1565512895395));
#16722=CARTESIAN_POINT('',(47.9470000000001,11.3549639738484,16.1565512895395));
#16723=CARTESIAN_POINT('',(384.,11.3549639738484,16.1565512895395));
#16724=CARTESIAN_POINT('Origin',(384.,13.3245794798728,16.5038476448733));
#16725=CARTESIAN_POINT('',(384.,11.9103659174997,15.0896340825003));
#16726=CARTESIAN_POINT('Origin',(384.,13.3245794798728,16.5038476448733));
#16727=CARTESIAN_POINT('',(47.9470000000001,11.9103659174997,15.0896340825003));
#16728=CARTESIAN_POINT('Origin',(47.9470000000001,13.3245794798728,16.5038476448733));
#16729=CARTESIAN_POINT('',(384.,11.9103659174997,15.0896340825003));
#16730=CARTESIAN_POINT('Origin',(384.,14.4142135623731,12.5857864376269));
#16731=CARTESIAN_POINT('',(384.,14.4142135623731,12.5857864376269));
#16732=CARTESIAN_POINT('',(384.,14.4142135623731,12.5857864376269));
#16733=CARTESIAN_POINT('',(47.9470000000001,14.4142135623731,12.5857864376269));
#16734=CARTESIAN_POINT('',(47.9470000000001,14.4142135623731,12.5857864376269));
#16735=CARTESIAN_POINT('',(384.,14.4142135623731,12.5857864376269));
#16736=CARTESIAN_POINT('Origin',(384.,15.8284271247462,14.));
#16737=CARTESIAN_POINT('Origin',(384.,15.8284271247462,14.));
#16738=CARTESIAN_POINT('Origin',(47.9470000000001,15.8284271247462,14.));
#16739=CARTESIAN_POINT('Origin',(384.,17.8849366916998,15.7373824589908));
#16740=CARTESIAN_POINT('Origin',(47.9470000000001,17.8849366916998,15.7373824589908));
#19194=UNCERTAINTY_MEASURE_WITH_UNIT(LENGTH_MEASURE(0.01),#19221,
'DISTANCE_ACCURACY_VALUE',
'Maximum model space distance between geometric entities at asserted c
onnectivities');
#19204=UNCERTAINTY_MEASURE_WITH_UNIT(LENGTH_MEASURE(0.01),#19221,
'DISTANCE_ACCURACY_VALUE',
'Maximum model space distance between geometric entities at asserted c
onnectivities');
#19210=(
GEOMETRIC_REPRESENTATION_CONTEXT(3)
GLOBAL_UNCERTAINTY_ASSIGNED_CONTEXT((#19194))
GLOBAL_UNIT_ASSIGNED_CONTEXT((#19221,#19223,#19224))
REPRESENTATION_CONTEXT('','3D')
);
#19220=(
GEOMETRIC_REPRESENTATION_CONTEXT(3)
GLOBAL_UNCERTAINTY_ASSIGNED_CONTEXT((#19204))
GLOBAL_UNIT_ASSIGNED_CONTEXT((#19221,#19223,#19224))
REPRESENTATION_CONTEXT('','3D')
);
#19221=(
LENGTH_UNIT()
NAMED_UNIT(*)
SI_UNIT(.MILLI.,.METRE.)
);
#19223=(
NAMED_UNIT(*)
PLANE_ANGLE_UNIT()
SI_UNIT($,.RADIAN.)
);
#19224=(
NAMED_UNIT(*)
SI_UNIT($,.STERADIAN.)
SOLID_ANGLE_UNIT()
);
#19230=SHAPE_DEFINITION_REPRESENTATION(#19245,#19274);
#19245=PRODUCT_DEFINITION_SHAPE('',$,#19290);
#19274=SHAPE_REPRESENTATION('',(#11684),#19210);
#19284=PRODUCT_DEFINITION_CONTEXT('part definition',#19331,'design');
#19290=PRODUCT_DEFINITION('Slider_01 (1)','Slider_01 (1)',#19305,#19284);
#19305=PRODUCT_DEFINITION_FORMATION('',$,#19338);
#19331=APPLICATION_CONTEXT(
'Core Data for Automotive Mechanical Design Process');
#19332=PRODUCT_CONTEXT('part definition',#19331,'mechanical');
#19338=PRODUCT('Slider_01 (1)','Slider_01 (1)',$,(#19332));
#19390=COLOUR_RGB('Sky Blue',0.24,0.69,0.87);
#19391=FILL_AREA_STYLE_COLOUR('',#19390);
#19392=FILL_AREA_STYLE('',(#19391));
#19393=SURFACE_STYLE_FILL_AREA(#19392);
#19394=SURFACE_SIDE_STYLE('',(#19393));
#19395=SURFACE_STYLE_USAGE(.BOTH.,#19394);
#19396=PRESENTATION_STYLE_ASSIGNMENT((#19395));
ENDSEC;
END-ISO-10303-21;
